ISO-10303-21;
HEADER;
FILE_DESCRIPTION (('STEP AP214'),
    '1' );
FILE_NAME ('spur gear_iso_ISO - Spur gear 2M 12T 20PA 8FW ---S12A75H50L8.0S1.step',
    '2026-09-28T15:49:00',
    ( '' ),
    ( '' ),
    'SwSTEP 2.0',
    'SolidWorks 2026',
    '' );
FILE_SCHEMA (( 'AUTOMOTIVE_DESIGN' ));
ENDSEC;

DATA;
#11=DIRECTION ( 'NONE',  ( 1.000000000000000000, -0.000000000000000000, -0.000000000000000000 ) ) ;
#28=DIRECTION ( 'NONE',  ( 0.000000000000000000, 0.000000000000000000, 1.000000000000000000 ) ) ;
#55=( NAMED_UNIT ( * ) SI_UNIT ( $, .STERADIAN. ) SOLID_ANGLE_UNIT ( ) );
#89=CYLINDRICAL_SURFACE ( 'NONE', #22796, 4.000000000000000000 ) ;
#104=ADVANCED_FACE ( 'NONE', ( #25008 ), #22116, .T. ) ;
#140=DIRECTION ( 'NONE',  ( -1.000000000000000000, 0.000000000000000000, 0.000000000000000000 ) ) ;
#173=ORIENTED_EDGE ( 'NONE', *, *, #35130, .T. ) ;
#219=VECTOR ( 'NONE', #13826, 1000.000000000000000 ) ;
#229=CARTESIAN_POINT ( 'NONE',  ( 0.000000000000000000, 9.919332006307222116, 5.363026430117163734 ) ) ;
#246=EDGE_LOOP ( 'NONE', ( #18364, #3419, #5510, #32868 ) ) ;
#252=DIRECTION ( 'NONE',  ( 0.000000000000000000, 0.000000000000000000, 1.000000000000000000 ) ) ;
#254=CARTESIAN_POINT ( 'NONE',  ( 0.000000000000000000, -9.604183132802424083, 5.908880290975512928 ) ) ;
#257=FACE_OUTER_BOUND ( 'NONE', #21375, .T. ) ;
#271=ORIENTED_EDGE ( 'NONE', *, *, #33716, .F. ) ;
#327=CARTESIAN_POINT ( 'NONE',  ( 50.00005079999998969, 5.400000000000098943, 1.000000000000000888 ) ) ;
#331=CARTESIAN_POINT ( 'NONE',  ( 50.00005079999998969, 5.400000000000029665, -1.000000000000000888 ) ) ;
#343=ORIENTED_EDGE ( 'NONE', *, *, #6840, .F. ) ;
#359=AXIS2_PLACEMENT_3D ( 'NONE', #30031, #5369, #29856 ) ;
#362=AXIS2_PLACEMENT_3D ( 'NONE', #20190, #31196, #14810 ) ;
#375=VERTEX_POINT ( 'NONE', #7637 ) ;
#409=CARTESIAN_POINT ( 'NONE',  ( 0.000000000000000000, -10.15474465512046542, 9.637487275701101197 ) ) ;
#442=AXIS2_PLACEMENT_3D ( 'NONE', #1395, #17763, #28764 ) ;
#455=LINE ( 'NONE', #30526, #1091 ) ;
#475=CARTESIAN_POINT ( 'NONE',  ( 8.000000000000007105, -5.363026430117185051, 9.919332006307207905 ) ) ;
#478=EDGE_CURVE ( 'NONE', #24108, #10834, #18807, .T. ) ;
#504=ORIENTED_EDGE ( 'NONE', *, *, #8965, .F. ) ;
#509=CARTESIAN_POINT ( 'NONE',  ( 0.000000000000000000, 0.000000000000000000, 4.000000000000000000 ) ) ;
#530=CARTESIAN_POINT ( 'NONE',  ( 8.000000000000007105, 11.27190672109280811, -0.3151488735047974776 ) ) ;
#544=EDGE_CURVE ( 'NONE', #34202, #2406, #30682, .T. ) ;
#577=VERTEX_POINT ( 'NONE', #17928 ) ;
#620=VERTEX_POINT ( 'NONE', #19503 ) ;
#631=EDGE_CURVE ( 'NONE', #27296, #14694, #28154, .T. ) ;
#640=CARTESIAN_POINT ( 'NONE',  ( 4.000000000000003553, -3.268936481846063113, -13.61301047812921183 ) ) ;
#646=AXIS2_PLACEMENT_3D ( 'NONE', #20529, #14704, #3938 ) ;
#669=ORIENTED_EDGE ( 'NONE', *, *, #23660, .F. ) ;
#677=PLANE ( 'NONE',  #20286 ) ;
#690=DIRECTION ( 'NONE',  ( -1.000000000000000000, 0.000000000000000000, 0.000000000000000000 ) ) ;
#694=CARTESIAN_POINT ( 'NONE',  ( 7.999999999999992895, 0.000000000000000000, 0.000000000000000000 ) ) ;
#716=VECTOR ( 'NONE', #27976, 1000.000000000000000 ) ;
#721=CIRCLE ( 'NONE', #4769, 4.800000000000005151 ) ;
#726=CARTESIAN_POINT ( 'NONE',  ( 8.000000000000007105, 9.919332006307222116, 5.363026430117163734 ) ) ;
#727=DIRECTION ( 'NONE',  ( -1.000000000000000000, 0.000000000000000000, 0.000000000000000000 ) ) ;
#741=VERTEX_POINT ( 'NONE', #14986 ) ;
#753=( NAMED_UNIT ( * ) SI_UNIT ( $, .STERADIAN. ) SOLID_ANGLE_UNIT ( ) );
#755=ORIENTED_EDGE ( 'NONE', *, *, #18321, .T. ) ;
#775=CIRCLE ( 'NONE', #20886, 9.499000000000012989 ) ;
#792=ORIENTED_EDGE ( 'NONE', *, *, #12344, .F. ) ;
#802=CARTESIAN_POINT ( 'NONE',  ( 8.000000000000007105, -11.27190672109260028, -0.3151488735048807444 ) ) ;
#816=FACE_OUTER_BOUND ( 'NONE', #2322, .T. ) ;
#826=EDGE_LOOP ( 'NONE', ( #7938, #26446, #19938, #30947 ) ) ;
#862=ORIENTED_EDGE ( 'NONE', *, *, #27591, .F. ) ;
#866=CARTESIAN_POINT ( 'NONE',  ( 0.000000000000000000, -8.725776631572701447, 3.753907720749016796 ) ) ;
#919=ORIENTED_EDGE ( 'NONE', *, *, #32387, .F. ) ;
#923=CYLINDRICAL_SURFACE ( 'NONE', #16159, 13.99999999999999822 ) ;
#949=VECTOR ( 'NONE', #32359, 1000.000000000000000 ) ;
#976=AXIS2_PLACEMENT_3D ( 'NONE', #5116, #7440, #29949 ) ;
#988=VECTOR ( 'NONE', #31472, 1000.000000000000000 ) ;
#1002=EDGE_CURVE ( 'NONE', #620, #27346, #26078, .T. ) ;
#1005=EDGE_CURVE ( 'NONE', #9557, #21816, #22163, .T. ) ;
#1023=CARTESIAN_POINT ( 'NONE',  ( 8.000000000000007105, -5.679790370315976666, -7.613867765417642097 ) ) ;
#1045=CARTESIAN_POINT ( 'NONE',  ( 8.000000000000007105, 7.613867765417711375, -5.679790370315948245 ) ) ;
#1087=EDGE_CURVE ( 'NONE', #7004, #1909, #24358, .T. ) ;
#1091=VECTOR ( 'NONE', #33567, 1000.000000000000000 ) ;
#1096=( LENGTH_UNIT ( ) NAMED_UNIT ( * ) SI_UNIT ( .MILLI., .METRE. ) );
#1117=ORIENTED_EDGE ( 'NONE', *, *, #9775, .T. ) ;
#1129=AXIS2_PLACEMENT_3D ( 'NONE', #2764, #24709, #30289 ) ;
#1144=CARTESIAN_POINT ( 'NONE',  ( 7.999999999999992895, 5.400000000000029665, -1.000000000000000888 ) ) ;
#1192=DIRECTION ( 'NONE',  ( -1.000000000000000000, 0.000000000000000000, 0.000000000000000000 ) ) ;
#1221=DIRECTION ( 'NONE',  ( 1.000000000000000000, -0.000000000000000000, 0.000000000000000000 ) ) ;
#1223=DIRECTION ( 'NONE',  ( -1.000000000000000000, 0.000000000000000000, 0.000000000000000000 ) ) ;
#1265=DIRECTION ( 'NONE',  ( -1.000000000000000000, 0.000000000000000000, 0.000000000000000000 ) ) ;
#1267=DIRECTION ( 'NONE',  ( 0.000000000000000000, -1.000000000000000000, -1.048062100069320848E-14 ) ) ;
#1276=CYLINDRICAL_SURFACE ( 'NONE', #10733, 4.800000000000000711 ) ;
#1293=EDGE_LOOP ( 'NONE', ( #32920, #21265, #23659, #24898 ) ) ;
#1300=VECTOR ( 'NONE', #31939, 1000.000000000000000 ) ;
#1316=EDGE_CURVE ( 'NONE', #24884, #17787, #25538, .T. ) ;
#1344=EDGE_CURVE ( 'NONE', #4384, #12104, #12293, .T. ) ;
#1367=DIRECTION ( 'NONE',  ( 0.000000000000000000, 0.000000000000000000, 1.000000000000000000 ) ) ;
#1371=DIRECTION ( 'NONE',  ( -1.000000000000000000, 0.000000000000000000, 0.000000000000000000 ) ) ;
#1395=CARTESIAN_POINT ( 'NONE',  ( 0.000000000000000000, 0.000000000000000000, 0.000000000000000000 ) ) ;
#1396=FACE_OUTER_BOUND ( 'NONE', #1571, .T. ) ;
#1400=CIRCLE ( 'NONE', #5998, 13.99999999999999645 ) ;
#1412=ORIENTED_EDGE ( 'NONE', *, *, #13569, .T. ) ;
#1435=EDGE_LOOP ( 'NONE', ( #7725, #862, #34876, #6549 ) ) ;
#1449=LINE ( 'NONE', #25771, #3133 ) ;
#1450=EDGE_CURVE ( 'NONE', #9747, #13957, #18039, .T. ) ;
#1457=FACE_OUTER_BOUND ( 'NONE', #826, .T. ) ;
#1461=DIRECTION ( 'NONE',  ( 0.000000000000000000, 0.000000000000000000, 1.000000000000000000 ) ) ;
#1482=AXIS2_PLACEMENT_3D ( 'NONE', #27649, #8181, #32491 ) ;
#1521=EDGE_CURVE ( 'NONE', #16008, #21028, #32422, .T. ) ;
#1534=ORIENTED_EDGE ( 'NONE', *, *, #24682, .F. ) ;
#1538=CIRCLE ( 'NONE', #6137, 4.800000000000002487 ) ;
#1552=VERTEX_POINT ( 'NONE', #10286 ) ;
#1556=AXIS2_PLACEMENT_3D ( 'NONE', #27267, #2609, #13056 ) ;
#1558=ORIENTED_EDGE ( 'NONE', *, *, #20914, .F. ) ;
#1565=AXIS2_PLACEMENT_3D ( 'NONE', #15918, #5489, #29982 ) ;
#1571=EDGE_LOOP ( 'NONE', ( #504, #10423, #21814, #16519 ) ) ;
#1572=ORIENTED_EDGE ( 'NONE', *, *, #10998, .F. ) ;
#1588=LINE ( 'NONE', #23359, #27447 ) ;
#1649=DIRECTION ( 'NONE',  ( -1.000000000000000000, 0.000000000000000000, 0.000000000000000000 ) ) ;
#1657=VERTEX_POINT ( 'NONE', #8794 ) ;
#1671=VECTOR ( 'NONE', #9095, 1000.000000000000000 ) ;
#1697=ORIENTED_EDGE ( 'NONE', *, *, #13227, .F. ) ;
#1705=DIRECTION ( 'NONE',  ( 0.000000000000000000, -0.8660254037844431485, 0.4999999999999921174 ) ) ;
#1712=DIRECTION ( 'NONE',  ( -1.000000000000000000, 0.000000000000000000, 0.000000000000000000 ) ) ;
#1748=CYLINDRICAL_SURFACE ( 'NONE', #21362, 9.499000000000000554 ) ;
#1784=ORIENTED_EDGE ( 'NONE', *, *, #30806, .F. ) ;
#1799=ADVANCED_FACE ( 'NONE', ( #12041 ), #23016, .T. ) ;
#1830=ADVANCED_FACE ( 'NONE', ( #28788 ), #26090, .T. ) ;
#1834=ORIENTED_EDGE ( 'NONE', *, *, #23660, .T. ) ;
#1842=CARTESIAN_POINT ( 'NONE',  ( 8.000000000000007105, -8.725776631572617958, -3.753907720749127819 ) ) ;
#1909=VERTEX_POINT ( 'NONE', #10590 ) ;
#1937=DIRECTION ( 'NONE',  ( 0.000000000000000000, 0.000000000000000000, 1.000000000000000000 ) ) ;
#1976=CIRCLE ( 'NONE', #33587, 4.800000000000000711 ) ;
#1984=DIRECTION ( 'NONE',  ( -1.000000000000000000, 0.000000000000000000, -0.000000000000000000 ) ) ;
#2029=EDGE_CURVE ( 'NONE', #10094, #13248, #18637, .T. ) ;
#2047=CARTESIAN_POINT ( 'NONE',  ( 8.000000000000007105, -7.613867765417531075, 5.679790370316011305 ) ) ;
#2051=CARTESIAN_POINT ( 'NONE',  ( 0.000000000000000000, 0.000000000000000000, -1.000000000000000888 ) ) ;
#2075=EDGE_CURVE ( 'NONE', #6952, #3956, #9457, .T. ) ;
#2078=CARTESIAN_POINT ( 'NONE',  ( 0.000000000000000000, -5.908880290975456973, -9.604183132802479150 ) ) ;
#2084=EDGE_CURVE ( 'NONE', #25259, #21336, #4883, .T. ) ;
#2110=CARTESIAN_POINT ( 'NONE',  ( 0.000000000000000000, 0.000000000000000000, 0.000000000000000000 ) ) ;
#2118=CIRCLE ( 'NONE', #30271, 4.800000000000005151 ) ;
#2121=FACE_OUTER_BOUND ( 'NONE', #15572, .T. ) ;
#2149=AXIS2_PLACEMENT_3D ( 'NONE', #20325, #28990, #26298 ) ;
#2151=AXIS2_PLACEMENT_3D ( 'NONE', #17549, #33959, #6233 ) ;
#2155=CIRCLE ( 'NONE', #32018, 4.800000000000000711 ) ;
#2189=CARTESIAN_POINT ( 'NONE',  ( 8.000000000000007105, 1.111908866155100650, 9.433698091065117808 ) ) ;
#2230=CARTESIAN_POINT ( 'NONE',  ( 8.000000000000007105, -8.725776631572701447, 3.753907720749016796 ) ) ;
#2234=DIRECTION ( 'NONE',  ( -1.000000000000000000, 0.000000000000000000, 0.000000000000000000 ) ) ;
#2236=AXIS2_PLACEMENT_3D ( 'NONE', #15972, #26802, #5204 ) ;
#2255=ORIENTED_EDGE ( 'NONE', *, *, #8629, .F. ) ;
#2262=DIRECTION ( 'NONE',  ( -1.000000000000000000, 0.000000000000000000, 0.000000000000000000 ) ) ;
#2266=DIRECTION ( 'NONE',  ( -0.000000000000000000, 1.000000000000000000, 0.000000000000000000 ) ) ;
#2322=EDGE_LOOP ( 'NONE', ( #32675, #6013, #15390, #21965 ) ) ;
#2345=FACE_OUTER_BOUND ( 'NONE', #31950, .T. ) ;
#2359=CARTESIAN_POINT ( 'NONE',  ( 0.000000000000000000, -5.908880290975582206, 9.604183132802395662 ) ) ;
#2404=LINE ( 'NONE', #13020, #8767 ) ;
#2406=VERTEX_POINT ( 'NONE', #3727 ) ;
#2448=DIRECTION ( 'NONE',  ( -1.000000000000000000, 0.000000000000000000, 0.000000000000000000 ) ) ;
#2452=CIRCLE ( 'NONE', #16207, 4.800000000000006040 ) ;
#2477=EDGE_CURVE ( 'NONE', #27617, #14457, #18543, .T. ) ;
#2536=FACE_OUTER_BOUND ( 'NONE', #20607, .T. ) ;
#2548=CARTESIAN_POINT ( 'NONE',  ( 8.000000000000007105, -9.919332006307138627, -5.363026430117212584 ) ) ;
#2558=CYLINDRICAL_SURFACE ( 'NONE', #34939, 4.800000000000000711 ) ;
#2560=CARTESIAN_POINT ( 'NONE',  ( 0.000000000000000000, -5.363026430117032284, -9.919332006307277183 ) ) ;
#2584=CARTESIAN_POINT ( 'NONE',  ( 8.000000000000007105, 0.3151488735048668666, 11.27190672109269798 ) ) ;
#2589=CARTESIAN_POINT ( 'NONE',  ( 8.000000000000007105, 5.363026430117226795, 9.919332006307262972 ) ) ;
#2609=DIRECTION ( 'NONE',  ( -1.000000000000000000, 0.000000000000000000, 0.000000000000000000 ) ) ;
#2623=DIRECTION ( 'NONE',  ( -1.000000000000000000, 0.000000000000000000, 0.000000000000000000 ) ) ;
#2632=ORIENTED_EDGE ( 'NONE', *, *, #28492, .T. ) ;
#2646=DIRECTION ( 'NONE',  ( -1.000000000000000000, 0.000000000000000000, 0.000000000000000000 ) ) ;
#2658=CARTESIAN_POINT ( 'NONE',  ( 8.000000000000007105, 5.908880290975540461, 9.604183132802438294 ) ) ;
#2667=CYLINDRICAL_SURFACE ( 'NONE', #18683, 4.800000000000000711 ) ;
#2744=ORIENTED_EDGE ( 'NONE', *, *, #29021, .F. ) ;
#2762=CYLINDRICAL_SURFACE ( 'NONE', #9475, 4.000000000000000000 ) ;
#2764=CARTESIAN_POINT ( 'NONE',  ( 0.000000000000000000, 9.919332006307387317, -5.363026430117004750 ) ) ;
#2776=DIRECTION ( 'NONE',  ( -1.000000000000000000, 0.000000000000000000, 0.000000000000000000 ) ) ;
#2782=ORIENTED_EDGE ( 'NONE', *, *, #11756, .T. ) ;
#2783=ORIENTED_EDGE ( 'NONE', *, *, #25393, .T. ) ;
#2803=CARTESIAN_POINT ( 'NONE',  ( 0.000000000000000000, 5.679790370316031733, 7.613867765417614564 ) ) ;
#2808=LINE ( 'NONE', #27101, #18817 ) ;
#2815=DIRECTION ( 'NONE',  ( 0.000000000000000000, -6.866613759074853001E-15, 1.000000000000000000 ) ) ;
#2820=ORIENTED_EDGE ( 'NONE', *, *, #11636, .F. ) ;
#2830=ORIENTED_EDGE ( 'NONE', *, *, #33480, .F. ) ;
#2844=CARTESIAN_POINT ( 'NONE',  ( 0.000000000000000000, 9.604183132802424083, -5.908880290975567995 ) ) ;
#2853=DIRECTION ( 'NONE',  ( 0.000000000000000000, 0.000000000000000000, -1.000000000000000000 ) ) ;
#2860=EDGE_CURVE ( 'NONE', #5109, #16923, #19694, .T. ) ;
#2867=AXIS2_PLACEMENT_3D ( 'NONE', #22513, #14409, #16756 ) ;
#2875=CARTESIAN_POINT ( 'NONE',  ( 8.000000000000007105, 9.637487275701129619, 10.15474465512053470 ) ) ;
#2908=LINE ( 'NONE', #11351, #30907 ) ;
#2914=CIRCLE ( 'NONE', #9205, 13.99999999999999645 ) ;
#2919=ORIENTED_EDGE ( 'NONE', *, *, #24743, .T. ) ;
#2928=CARTESIAN_POINT ( 'NONE',  ( 8.000000000000007105, 0.000000000000000000, 0.000000000000000000 ) ) ;
#2933=ADVANCED_FACE ( 'NONE', ( #32112 ), #31924, .T. ) ;
#2934=DIRECTION ( 'NONE',  ( -1.000000000000000000, 0.000000000000000000, 0.000000000000000000 ) ) ;
#2937=AXIS2_PLACEMENT_3D ( 'NONE', #2844, #32715, #21899 ) ;
#2949=CARTESIAN_POINT ( 'NONE',  ( 0.000000000000000000, 5.908880290975540461, 9.604183132802438294 ) ) ;
#2969=ADVANCED_FACE ( 'NONE', ( #34644 ), #29055, .T. ) ;
#2971=FACE_OUTER_BOUND ( 'NONE', #8027, .T. ) ;
#2982=LINE ( 'NONE', #27982, #7786 ) ;
#2997=AXIS2_PLACEMENT_3D ( 'NONE', #14692, #34519, #34159 ) ;
#3002=DIRECTION ( 'NONE',  ( 0.000000000000000000, 0.000000000000000000, 1.000000000000000000 ) ) ;
#3009=EDGE_CURVE ( 'NONE', #6246, #26745, #775, .T. ) ;
#3010=CARTESIAN_POINT ( 'NONE',  ( 8.000000000000007105, 13.61301047812919052, -3.268936481846215880 ) ) ;
#3011=AXIS2_PLACEMENT_3D ( 'NONE', #7848, #24423, #35412 ) ;
#3033=LINE ( 'NONE', #19395, #219 ) ;
#3069=ORIENTED_EDGE ( 'NONE', *, *, #32265, .T. ) ;
#3094=EDGE_CURVE ( 'NONE', #19486, #16196, #9900, .T. ) ;
#3133=VECTOR ( 'NONE', #26486, 1000.000000000000000 ) ;
#3149=CARTESIAN_POINT ( 'NONE',  ( 4.000000000000003553, 9.637487275701115408, 10.15474465512054181 ) ) ;
#3165=AXIS2_PLACEMENT_3D ( 'NONE', #18183, #21055, #4543 ) ;
#3169=CARTESIAN_POINT ( 'NONE',  ( 8.000000000000007105, -9.604183132802424083, 5.908880290975512928 ) ) ;
#3172=CARTESIAN_POINT ( 'NONE',  ( 8.000000000000007105, 13.61301047812928111, 3.268936481846215880 ) ) ;
#3194=DIRECTION ( 'NONE',  ( -1.000000000000000000, 0.000000000000000000, 0.000000000000000000 ) ) ;
#3197=ORIENTED_EDGE ( 'NONE', *, *, #14695, .T. ) ;
#3227=LINE ( 'NONE', #14012, #19913 ) ;
#3259=CIRCLE ( 'NONE', #359, 4.800000000000000711 ) ;
#3281=VECTOR ( 'NONE', #13675, 1000.000000000000000 ) ;
#3293=DIRECTION ( 'NONE',  ( -1.000000000000000000, 0.000000000000000000, 0.000000000000000000 ) ) ;
#3314=CARTESIAN_POINT ( 'NONE',  ( 0.000000000000000000, 5.679790370316226245, -7.613867765417517752 ) ) ;
#3326=CARTESIAN_POINT ( 'NONE',  ( 8.000000000000007105, 11.27190672109280811, 4.484851126495202678 ) ) ;
#3329=ORIENTED_EDGE ( 'NONE', *, *, #22946, .F. ) ;
#3354=DIRECTION ( 'NONE',  ( 0.000000000000000000, 0.000000000000000000, 1.000000000000000000 ) ) ;
#3418=CARTESIAN_POINT ( 'NONE',  ( 0.000000000000000000, 0.000000000000000000, 0.000000000000000000 ) ) ;
#3419=ORIENTED_EDGE ( 'NONE', *, *, #22946, .T. ) ;
#3427=DIRECTION ( 'NONE',  ( 0.000000000000000000, 0.5000000000000011102, -0.8660254037844379305 ) ) ;
#3433=ORIENTED_EDGE ( 'NONE', *, *, #12611, .F. ) ;
#3467=CARTESIAN_POINT ( 'NONE',  ( 8.000000000000007105, -9.433698091065020108, -1.111908866155191022 ) ) ;
#3470=DIRECTION ( 'NONE',  ( 0.000000000000000000, 1.000000000000000000, 3.614007241618346010E-15 ) ) ;
#3516=ORIENTED_EDGE ( 'NONE', *, *, #4525, .F. ) ;
#3520=DIRECTION ( 'NONE',  ( 0.000000000000000000, 0.000000000000000000, 1.000000000000000000 ) ) ;
#3523=AXIS2_PLACEMENT_3D ( 'NONE', #4514, #4146, #12406 ) ;
#3535=EDGE_CURVE ( 'NONE', #23109, #26849, #20321, .T. ) ;
#3572=LINE ( 'NONE', #19915, #20758 ) ;
#3587=ORIENTED_EDGE ( 'NONE', *, *, #34796, .F. ) ;
#3652=FILL_AREA_STYLE_COLOUR ( '', #21906 ) ;
#3661=ORIENTED_EDGE ( 'NONE', *, *, #6649, .T. ) ;
#3677=VERTEX_POINT ( 'NONE', #9890 ) ;
#3693=ORIENTED_EDGE ( 'NONE', *, *, #31526, .F. ) ;
#3699=CARTESIAN_POINT ( 'NONE',  ( 50.00005079999998969, 3.872983346207531596, 1.000000000000000888 ) ) ;
#3712=DIRECTION ( 'NONE',  ( 0.000000000000000000, -0.8660254037844326014, -0.5000000000000102141 ) ) ;
#3713=DIRECTION ( 'NONE',  ( 1.000000000000000000, -0.000000000000000000, 0.000000000000000000 ) ) ;
#3719=ORIENTED_EDGE ( 'NONE', *, *, #8829, .T. ) ;
#3725=VERTEX_POINT ( 'NONE', #33854 ) ;
#3727=CARTESIAN_POINT ( 'NONE',  ( 0.000000000000000000, 5.400000000000029665, -1.000000000000000888 ) ) ;
#3731=ADVANCED_FACE ( 'NONE', ( #9180 ), #20144, .T. ) ;
#3732=FACE_OUTER_BOUND ( 'NONE', #22735, .T. ) ;
#3740=FACE_OUTER_BOUND ( 'NONE', #13159, .T. ) ;
#3776=VECTOR ( 'NONE', #16093, 1000.000000000000000 ) ;
#3778=EDGE_CURVE ( 'NONE', #10834, #18507, #7072, .T. ) ;
#3807=ORIENTED_EDGE ( 'NONE', *, *, #14980, .T. ) ;
#3817=FACE_OUTER_BOUND ( 'NONE', #18834, .T. ) ;
#3826=ORIENTED_EDGE ( 'NONE', *, *, #33672, .T. ) ;
#3873=VERTEX_POINT ( 'NONE', #10796 ) ;
#3886=CARTESIAN_POINT ( 'NONE',  ( -9.999999999999994671, 0.000000000000000000, 0.000000000000000000 ) ) ;
#3888=AXIS2_PLACEMENT_3D ( 'NONE', #21872, #29638, #24069 ) ;
#3889=DIRECTION ( 'NONE',  ( 0.000000000000000000, 0.000000000000000000, 1.000000000000000000 ) ) ;
#3898=DIRECTION ( 'NONE',  ( 0.000000000000000000, 0.000000000000000000, 1.000000000000000000 ) ) ;
#3938=DIRECTION ( 'NONE',  ( 0.000000000000000000, 0.000000000000000000, 1.000000000000000000 ) ) ;
#3943=CYLINDRICAL_SURFACE ( 'NONE', #10566, 4.800000000000000711 ) ;
#3944=DIRECTION ( 'NONE',  ( -1.000000000000000000, 0.000000000000000000, 0.000000000000000000 ) ) ;
#3956=VERTEX_POINT ( 'NONE', #30233 ) ;
#3958=DIRECTION ( 'NONE',  ( -1.000000000000000000, 0.000000000000000000, 0.000000000000000000 ) ) ;
#3977=CARTESIAN_POINT ( 'NONE',  ( 4.000000000000003553, -13.61301047812919762, 3.268936481846118625 ) ) ;
#3998=ADVANCED_FACE ( 'NONE', ( #16876 ), #677, .T. ) ;
#4004=LINE ( 'NONE', #7208, #22490 ) ;
#4007=ORIENTED_EDGE ( 'NONE', *, *, #2084, .T. ) ;
#4064=AXIS2_PLACEMENT_3D ( 'NONE', #2078, #10162, #24205 ) ;
#4146=DIRECTION ( 'NONE',  ( -1.000000000000000000, 0.000000000000000000, 0.000000000000000000 ) ) ;
#4178=CARTESIAN_POINT ( 'NONE',  ( 8.000000000000007105, 0.000000000000000000, 0.000000000000000000 ) ) ;
#4196=ADVANCED_FACE ( 'NONE', ( #12206 ), #33817, .T. ) ;
#4205=DIRECTION ( 'NONE',  ( -1.000000000000000000, 0.000000000000000000, 0.000000000000000000 ) ) ;
#4217=ORIENTED_EDGE ( 'NONE', *, *, #22440, .F. ) ;
#4253=DIRECTION ( 'NONE',  ( -1.000000000000000000, 0.000000000000000000, 0.000000000000000000 ) ) ;
#4265=EDGE_CURVE ( 'NONE', #3873, #375, #11694, .T. ) ;
#4267=ORIENTED_EDGE ( 'NONE', *, *, #7475, .F. ) ;
#4269=CARTESIAN_POINT ( 'NONE',  ( 0.000000000000000000, 5.400000000000098943, 1.000000000000000888 ) ) ;
#4276=CARTESIAN_POINT ( 'NONE',  ( 0.000000000000000000, 3.268936481846187903, 13.61301047812924025 ) ) ;
#4354=FACE_OUTER_BOUND ( 'NONE', #29347, .T. ) ;
#4370=PRODUCT_DEFINITION_SHAPE ( 'NONE', 'NONE',  #32378 ) ;
#4382=DIRECTION ( 'NONE',  ( 0.000000000000000000, 0.000000000000000000, 1.000000000000000000 ) ) ;
#4384=VERTEX_POINT ( 'NONE', #3010 ) ;
#4450=AXIS2_PLACEMENT_3D ( 'NONE', #5826, #33365, #30668 ) ;
#4473=CIRCLE ( 'NONE', #32060, 4.800000000000006040 ) ;
#4492=ORIENTED_EDGE ( 'NONE', *, *, #35130, .F. ) ;
#4514=CARTESIAN_POINT ( 'NONE',  ( -9.999999999999994671, 0.000000000000000000, 0.000000000000000000 ) ) ;
#4525=EDGE_CURVE ( 'NONE', #10473, #7400, #27265, .T. ) ;
#4543=DIRECTION ( 'NONE',  ( 0.000000000000000000, 0.5000000000000011102, -0.8660254037844379305 ) ) ;
#4577=CARTESIAN_POINT ( 'NONE',  ( 0.000000000000000000, 3.872983346207420574, -1.000000000000000888 ) ) ;
#4580=DIRECTION ( 'NONE',  ( 0.000000000000000000, 0.000000000000000000, -1.000000000000000000 ) ) ;
#4596=DIRECTION ( 'NONE',  ( -1.000000000000000000, 0.000000000000000000, 0.000000000000000000 ) ) ;
#4608=AXIS2_PLACEMENT_3D ( 'NONE', #11139, #16868, #25182 ) ;
#4624=ORIENTED_EDGE ( 'NONE', *, *, #31983, .T. ) ;
#4674=EDGE_LOOP ( 'NONE', ( #27595, #20983, #3661, #23050 ) ) ;
#4697=CARTESIAN_POINT ( 'NONE',  ( 8.000000000000007105, 3.753907720749127819, 8.725776631572756514 ) ) ;
#4719=AXIS2_PLACEMENT_3D ( 'NONE', #33993, #1223, #25359 ) ;
#4764=DIRECTION ( 'NONE',  ( -1.000000000000000000, 0.000000000000000000, 0.000000000000000000 ) ) ;
#4769=AXIS2_PLACEMENT_3D ( 'NONE', #29069, #23847, #5132 ) ;
#4790=CARTESIAN_POINT ( 'NONE',  ( 8.000000000000007105, -9.919332006307262972, 5.363026430117087351 ) ) ;
#4809=ORIENTED_EDGE ( 'NONE', *, *, #18799, .T. ) ;
#4842=FACE_OUTER_BOUND ( 'NONE', #15782, .T. ) ;
#4850=EDGE_CURVE ( 'NONE', #13312, #3956, #1400, .T. ) ;
#4875=DIRECTION ( 'NONE',  ( 0.000000000000000000, 0.000000000000000000, -1.000000000000000000 ) ) ;
#4883=CIRCLE ( 'NONE', #20959, 4.800000000000002487 ) ;
#4900=DIRECTION ( 'NONE',  ( 0.000000000000000000, 0.000000000000000000, -1.000000000000000000 ) ) ;
#4914=EDGE_CURVE ( 'NONE', #33676, #29329, #1449, .T. ) ;
#4925=CIRCLE ( 'NONE', #19833, 4.800000000000000711 ) ;
#4931=EDGE_CURVE ( 'NONE', #10012, #34823, #7149, .T. ) ;
#4947=DIRECTION ( 'NONE',  ( -1.000000000000000000, 0.000000000000000000, 0.000000000000000000 ) ) ;
#4955=CIRCLE ( 'NONE', #34296, 4.800000000000003375 ) ;
#4964=EDGE_LOOP ( 'NONE', ( #23071, #23246, #173, #15881 ) ) ;
#4966=CYLINDRICAL_SURFACE ( 'NONE', #16975, 4.799999999999998934 ) ;
#4980=ORIENTED_EDGE ( 'NONE', *, *, #11686, .F. ) ;
#4998=CARTESIAN_POINT ( 'NONE',  ( 0.000000000000000000, 9.637487275701349887, -10.15474465512039615 ) ) ;
#5010=ORIENTED_EDGE ( 'NONE', *, *, #16114, .F. ) ;
#5011=EDGE_CURVE ( 'NONE', #13957, #10771, #1976, .T. ) ;
#5016=DIRECTION ( 'NONE',  ( -1.000000000000000000, 0.000000000000000000, 0.000000000000000000 ) ) ;
#5021=DIRECTION ( 'NONE',  ( -1.000000000000000000, 0.000000000000000000, 0.000000000000000000 ) ) ;
#5025=ORIENTED_EDGE ( 'NONE', *, *, #12344, .T. ) ;
#5027=DIRECTION ( 'NONE',  ( -1.000000000000000000, 0.000000000000000000, 0.000000000000000000 ) ) ;
#5032=ORIENTED_EDGE ( 'NONE', *, *, #26877, .F. ) ;
#5046=EDGE_CURVE ( 'NONE', #3725, #12104, #29542, .T. ) ;
#5050=DIRECTION ( 'NONE',  ( 0.000000000000000000, -0.8660254037844327124, -0.5000000000000102141 ) ) ;
#5068=CARTESIAN_POINT ( 'NONE',  ( 8.000000000000007105, 9.919332006307387317, -5.363026430117004750 ) ) ;
#5079=CIRCLE ( 'NONE', #6215, 4.000000000000000000 ) ;
#5088=EDGE_CURVE ( 'NONE', #15252, #22087, #16332, .T. ) ;
#5109=VERTEX_POINT ( 'NONE', #16175 ) ;
#5116=CARTESIAN_POINT ( 'NONE',  ( 8.000000000000007105, 0.000000000000000000, 0.000000000000000000 ) ) ;
#5130=ADVANCED_FACE ( 'NONE', ( #2536 ), #21411, .T. ) ;
#5132=DIRECTION ( 'NONE',  ( 0.000000000000000000, 0.4999999999999951150, 0.8660254037844414832 ) ) ;
#5140=DIRECTION ( 'NONE',  ( -1.000000000000000000, 0.000000000000000000, 0.000000000000000000 ) ) ;
#5164=ORIENTED_EDGE ( 'NONE', *, *, #31526, .T. ) ;
#5172=PLANE ( 'NONE',  #19101 ) ;
#5204=DIRECTION ( 'NONE',  ( 0.000000000000000000, 0.000000000000000000, 1.000000000000000000 ) ) ;
#5223=DIRECTION ( 'NONE',  ( -1.000000000000000000, 0.000000000000000000, 0.000000000000000000 ) ) ;
#5264=EDGE_LOOP ( 'NONE', ( #32286, #15409, #28994, #19073 ) ) ;
#5281=DIRECTION ( 'NONE',  ( 0.000000000000000000, 0.000000000000000000, 1.000000000000000000 ) ) ;
#5297=EDGE_LOOP ( 'NONE', ( #4980, #5563, #26332, #12257 ) ) ;
#5312=DIRECTION ( 'NONE',  ( -1.000000000000000000, 0.000000000000000000, 0.000000000000000000 ) ) ;
#5321=EDGE_LOOP ( 'NONE', ( #17064, #15114, #2783, #31356 ) ) ;
#5325=CARTESIAN_POINT ( 'NONE',  ( 8.000000000000007105, 9.604183132802424083, -1.108880290975567950 ) ) ;
#5368=CARTESIAN_POINT ( 'NONE',  ( 8.000000000000007105, -1.111908866155017606, -9.433698091065132019 ) ) ;
#5369=DIRECTION ( 'NONE',  ( -1.000000000000000000, 0.000000000000000000, 0.000000000000000000 ) ) ;
#5400=LINE ( 'NONE', #22465, #3281 ) ;
#5406=DIRECTION ( 'NONE',  ( 1.000000000000000000, -0.000000000000000000, 0.000000000000000000 ) ) ;
#5408=ORIENTED_EDGE ( 'NONE', *, *, #9207, .F. ) ;
#5417=DIRECTION ( 'NONE',  ( 0.000000000000000000, 0.000000000000000000, -1.000000000000000000 ) ) ;
#5429=ORIENTED_EDGE ( 'NONE', *, *, #23302, .F. ) ;
#5451=ORIENTED_EDGE ( 'NONE', *, *, #3535, .T. ) ;
#5472=VECTOR ( 'NONE', #28959, 1000.000000000000000 ) ;
#5489=DIRECTION ( 'NONE',  ( -1.000000000000000000, 0.000000000000000000, 0.000000000000000000 ) ) ;
#5510=ORIENTED_EDGE ( 'NONE', *, *, #30673, .F. ) ;
#5520=AXIS2_PLACEMENT_3D ( 'NONE', #8524, #25985, #14978 ) ;
#5522=CARTESIAN_POINT ( 'NONE',  ( 0.000000000000000000, 7.613867765417711375, -5.679790370315948245 ) ) ;
#5540=CARTESIAN_POINT ( 'NONE',  ( 8.000000000000007105, 9.433698091065187086, -1.111908866155128628 ) ) ;
#5563=ORIENTED_EDGE ( 'NONE', *, *, #32159, .T. ) ;
#5585=VECTOR ( 'NONE', #20536, 1000.000000000000000 ) ;
#5595=AXIS2_PLACEMENT_3D ( 'NONE', #24655, #19577, #27545 ) ;
#5605=ORIENTED_EDGE ( 'NONE', *, *, #34796, .T. ) ;
#5615=CARTESIAN_POINT ( 'NONE',  ( 8.000000000000007105, 5.679790370316226245, -7.613867765417517752 ) ) ;
#5624=DIRECTION ( 'NONE',  ( -1.000000000000000000, 0.000000000000000000, 0.000000000000000000 ) ) ;
#5625=CIRCLE ( 'NONE', #442, 13.99999999999999645 ) ;
#5632=DIRECTION ( 'NONE',  ( -1.000000000000000000, 0.000000000000000000, 0.000000000000000000 ) ) ;
#5645=FILL_AREA_STYLE ('',( #3652 ) ) ;
#5651=DIRECTION ( 'NONE',  ( 0.000000000000000000, 0.000000000000000000, 1.000000000000000000 ) ) ;
#5674=CARTESIAN_POINT ( 'NONE',  ( 8.000000000000007105, 8.725776631572770725, -3.753907720748954180 ) ) ;
#5769=CYLINDRICAL_SURFACE ( 'NONE', #29225, 4.800000000000000711 ) ;
#5770=ORIENTED_EDGE ( 'NONE', *, *, #12555, .T. ) ;
#5790=ADVANCED_FACE ( 'NONE', ( #19538 ), #2667, .T. ) ;
#5826=CARTESIAN_POINT ( 'NONE',  ( 0.000000000000000000, -0.3151488735047419665, 11.27190672109269798 ) ) ;
#5844=LINE ( 'NONE', #5674, #13272 ) ;
#5845=VECTOR ( 'NONE', #35076, 1000.000000000000000 ) ;
#5881=DIRECTION ( 'NONE',  ( 0.000000000000000000, 0.000000000000000000, -1.000000000000000000 ) ) ;
#5891=EDGE_CURVE ( 'NONE', #21028, #35157, #12971, .T. ) ;
#5916=CARTESIAN_POINT ( 'NONE',  ( 0.000000000000000000, -3.975523202427916125, -13.42368113696676346 ) ) ;
#5918=VECTOR ( 'NONE', #21678, 1000.000000000000000 ) ;
#5995=ADVANCED_FACE ( 'NONE', ( #816 ), #25868, .T. ) ;
#5998=AXIS2_PLACEMENT_3D ( 'NONE', #20151, #5140, #16079 ) ;
#6013=ORIENTED_EDGE ( 'NONE', *, *, #14923, .F. ) ;
#6017=DIRECTION ( 'NONE',  ( -1.000000000000000000, 0.000000000000000000, 0.000000000000000000 ) ) ;
#6027=ORIENTED_EDGE ( 'NONE', *, *, #4850, .T. ) ;
#6033=FACE_OUTER_BOUND ( 'NONE', #12968, .T. ) ;
#6038=ADVANCED_FACE ( 'NONE', ( #9997 ), #4966, .T. ) ;
#6069=EDGE_LOOP ( 'NONE', ( #22792, #11645, #3433, #14289 ) ) ;
#6081=ORIENTED_EDGE ( 'NONE', *, *, #19863, .T. ) ;
#6111=DIRECTION ( 'NONE',  ( 0.000000000000000000, 0.000000000000000000, 1.000000000000000000 ) ) ;
#6137=AXIS2_PLACEMENT_3D ( 'NONE', #2949, #16938, #3470 ) ;
#6144=DIRECTION ( 'NONE',  ( 0.000000000000000000, 0.5000000000000011102, -0.8660254037844379305 ) ) ;
#6153=LINE ( 'NONE', #3467, #8439 ) ;
#6202=CARTESIAN_POINT ( 'NONE',  ( 8.000000000000007105, 13.42368113696682030, 3.975523202428055125 ) ) ;
#6211=VECTOR ( 'NONE', #10954, 1000.000000000000000 ) ;
#6215=AXIS2_PLACEMENT_3D ( 'NONE', #694, #19592, #14728 ) ;
#6233=DIRECTION ( 'NONE',  ( 0.000000000000000000, 0.4999999999999948930, 0.8660254037844415942 ) ) ;
#6246=VERTEX_POINT ( 'NONE', #32857 ) ;
#6251=EDGE_CURVE ( 'NONE', #28225, #14425, #2982, .T. ) ;
#6252=AXIS2_PLACEMENT_3D ( 'NONE', #3169, #30703, #3520 ) ;
#6262=CARTESIAN_POINT ( 'NONE',  ( 8.000000000000007105, 9.604183132802452505, 5.908880290975567995 ) ) ;
#6287=VERTEX_POINT ( 'NONE', #13590 ) ;
#6323=CARTESIAN_POINT ( 'NONE',  ( -9.999999999999994671, 0.000000000000000000, 0.000000000000000000 ) ) ;
#6332=ORIENTED_EDGE ( 'NONE', *, *, #11686, .T. ) ;
#6336=AXIS2_PLACEMENT_3D ( 'NONE', #19763, #28926, #26223 ) ;
#6381=ORIENTED_EDGE ( 'NONE', *, *, #1344, .T. ) ;
#6384=VECTOR ( 'NONE', #11832, 1000.000000000000000 ) ;
#6395=EDGE_LOOP ( 'NONE', ( #22688, #31988, #1697, #34465 ) ) ;
#6411=CARTESIAN_POINT ( 'NONE',  ( 8.000000000000007105, -9.919332006307138627, -5.363026430117212584 ) ) ;
#6420=DIRECTION ( 'NONE',  ( 0.000000000000000000, 0.000000000000000000, 1.000000000000000000 ) ) ;
#6422=SHAPE_DEFINITION_REPRESENTATION ( #4370, #22901 ) ;
#6425=VERTEX_POINT ( 'NONE', #12299 ) ;
#6434=LINE ( 'NONE', #14519, #6384 ) ;
#6438=DIRECTION ( 'NONE',  ( 0.000000000000000000, 0.000000000000000000, 1.000000000000000000 ) ) ;
#6468=LINE ( 'NONE', #26098, #20166 ) ;
#6479=AXIS2_PLACEMENT_3D ( 'NONE', #13154, #16168, #5050 ) ;
#6509=LINE ( 'NONE', #29016, #31671 ) ;
#6517=DIRECTION ( 'NONE',  ( -1.000000000000000000, 0.000000000000000000, 0.000000000000000000 ) ) ;
#6542=DIRECTION ( 'NONE',  ( 1.000000000000000000, -0.000000000000000000, -0.000000000000000000 ) ) ;
#6549=ORIENTED_EDGE ( 'NONE', *, *, #16114, .T. ) ;
#6559=CARTESIAN_POINT ( 'NONE',  ( 8.000000000000007105, 0.000000000000000000, 0.000000000000000000 ) ) ;
#6576=CYLINDRICAL_SURFACE ( 'NONE', #34517, 9.499000000000000554 ) ;
#6586=ORIENTED_EDGE ( 'NONE', *, *, #29021, .T. ) ;
#6604=ORIENTED_EDGE ( 'NONE', *, *, #29132, .T. ) ;
#6628=ORIENTED_EDGE ( 'NONE', *, *, #13462, .F. ) ;
#6635=EDGE_CURVE ( 'NONE', #25674, #1552, #35001, .T. ) ;
#6638=EDGE_CURVE ( 'NONE', #2406, #22936, #7071, .T. ) ;
#6649=EDGE_CURVE ( 'NONE', #19114, #20656, #17591, .T. ) ;
#6672=CARTESIAN_POINT ( 'NONE',  ( 0.000000000000000000, 9.433698091065215507, 1.111908866155128628 ) ) ;
#6688=CIRCLE ( 'NONE', #20471, 4.800000000000005151 ) ;
#6699=EDGE_CURVE ( 'NONE', #6952, #33344, #32540, .T. ) ;
#6701=DIRECTION ( 'NONE',  ( 0.000000000000000000, 0.000000000000000000, 1.000000000000000000 ) ) ;
#6725=ORIENTED_EDGE ( 'NONE', *, *, #12153, .T. ) ;
#6746=CYLINDRICAL_SURFACE ( 'NONE', #6819, 9.499000000000000554 ) ;
#6758=DIRECTION ( 'NONE',  ( 0.000000000000000000, -0.4999999999999888978, -0.8660254037844450359 ) ) ;
#6819=AXIS2_PLACEMENT_3D ( 'NONE', #6559, #17534, #3889 ) ;
#6830=DIRECTION ( 'NONE',  ( -1.000000000000000000, 0.000000000000000000, 0.000000000000000000 ) ) ;
#6840=EDGE_CURVE ( 'NONE', #22842, #3725, #15846, .T. ) ;
#6845=DIRECTION ( 'NONE',  ( -1.000000000000000000, 0.000000000000000000, 0.000000000000000000 ) ) ;
#6858=EDGE_CURVE ( 'NONE', #15170, #3677, #4955, .T. ) ;
#6881=CARTESIAN_POINT ( 'NONE',  ( 0.000000000000000000, 0.000000000000000000, 0.000000000000000000 ) ) ;
#6952=VERTEX_POINT ( 'NONE', #6672 ) ;
#6980=CARTESIAN_POINT ( 'NONE',  ( 7.999999999999992895, 0.000000000000000000, 4.000000000000000000 ) ) ;
#7004=VERTEX_POINT ( 'NONE', #33682 ) ;
#7017=ORIENTED_EDGE ( 'NONE', *, *, #4914, .T. ) ;
#7049=ORIENTED_EDGE ( 'NONE', *, *, #3009, .F. ) ;
#7051=ORIENTED_EDGE ( 'NONE', *, *, #2860, .T. ) ;
#7053=ADVANCED_FACE ( 'NONE', ( #14771 ), #1276, .T. ) ;
#7060=FACE_OUTER_BOUND ( 'NONE', #22430, .T. ) ;
#7067=CARTESIAN_POINT ( 'NONE',  ( 8.000000000000007105, 0.000000000000000000, 0.000000000000000000 ) ) ;
#7071=LINE ( 'NONE', #2051, #27396 ) ;
#7072=CIRCLE ( 'NONE', #6479, 4.800000000000002487 ) ;
#7100=EDGE_CURVE ( 'NONE', #27258, #29830, #3259, .T. ) ;
#7123=APPLICATION_CONTEXT ( 'automotive_design' ) ;
#7131=ADVANCED_FACE ( 'NONE', ( #1457 ), #16316, .T. ) ;
#7149=CIRCLE ( 'NONE', #15746, 4.000000000000000000 ) ;
#7188=DIRECTION ( 'NONE',  ( -1.000000000000000000, 0.000000000000000000, 0.000000000000000000 ) ) ;
#7196=DIRECTION ( 'NONE',  ( 0.000000000000000000, 0.000000000000000000, 1.000000000000000000 ) ) ;
#7208=CARTESIAN_POINT ( 'NONE',  ( 8.000000000000007105, 0.000000000000000000, 9.499000000000000554 ) ) ;
#7217=ORIENTED_EDGE ( 'NONE', *, *, #2084, .F. ) ;
#7222=ORIENTED_EDGE ( 'NONE', *, *, #17374, .F. ) ;
#7248=VECTOR ( 'NONE', #10131, 1000.000000000000000 ) ;
#7253=AXIS2_PLACEMENT_3D ( 'NONE', #26527, #29227, #4382 ) ;
#7256=AXIS2_PLACEMENT_3D ( 'NONE', #25644, #9250, #31573 ) ;
#7257=LINE ( 'NONE', #17516, #7826 ) ;
#7318=EDGE_LOOP ( 'NONE', ( #12183, #5164, #7561, #27596 ) ) ;
#7319=AXIS2_PLACEMENT_3D ( 'NONE', #13739, #2776, #32995 ) ;
#7363=ORIENTED_EDGE ( 'NONE', *, *, #19417, .F. ) ;
#7400=VERTEX_POINT ( 'NONE', #21847 ) ;
#7440=DIRECTION ( 'NONE',  ( -1.000000000000000000, 0.000000000000000000, 0.000000000000000000 ) ) ;
#7460=EDGE_CURVE ( 'NONE', #23680, #16526, #7863, .T. ) ;
#7461=DIRECTION ( 'NONE',  ( 0.000000000000000000, -0.8660254037844327124, -0.5000000000000104361 ) ) ;
#7475=EDGE_CURVE ( 'NONE', #24024, #9557, #27092, .T. ) ;
#7524=ORIENTED_EDGE ( 'NONE', *, *, #26877, .T. ) ;
#7527=CYLINDRICAL_SURFACE ( 'NONE', #2236, 4.800000000000000711 ) ;
#7558=DIRECTION ( 'NONE',  ( 0.000000000000000000, 0.000000000000000000, -1.000000000000000000 ) ) ;
#7561=ORIENTED_EDGE ( 'NONE', *, *, #15830, .T. ) ;
#7573=CARTESIAN_POINT ( 'NONE',  ( 8.000000000000007105, -9.637487275701184686, 10.15474465512046542 ) ) ;
#7577=EDGE_CURVE ( 'NONE', #21336, #14025, #17652, .T. ) ;
#7627=EDGE_CURVE ( 'NONE', #6287, #14457, #25720, .T. ) ;
#7637=CARTESIAN_POINT ( 'NONE',  ( 0.000000000000000000, -1.111908866155017606, -9.433698091065132019 ) ) ;
#7672=AXIS2_PLACEMENT_3D ( 'NONE', #11835, #27878, #23179 ) ;
#7689=CARTESIAN_POINT ( 'NONE',  ( 8.000000000000007105, 0.000000000000000000, 0.000000000000000000 ) ) ;
#7725=ORIENTED_EDGE ( 'NONE', *, *, #4265, .F. ) ;
#7747=ORIENTED_EDGE ( 'NONE', *, *, #32341, .F. ) ;
#7751=DIRECTION ( 'NONE',  ( 1.000000000000000000, -0.000000000000000000, 0.000000000000000000 ) ) ;
#7786=VECTOR ( 'NONE', #35574, 1000.000000000000000 ) ;
#7825=CARTESIAN_POINT ( 'NONE',  ( 8.000000000000007105, 9.637487275701364098, -10.15474465512039615 ) ) ;
#7826=VECTOR ( 'NONE', #6542, 1000.000000000000000 ) ;
#7827=LINE ( 'NONE', #30345, #3776 ) ;
#7848=CARTESIAN_POINT ( 'NONE',  ( 8.000000000000007105, 0.000000000000000000, 0.000000000000000000 ) ) ;
#7851=AXIS2_PLACEMENT_3D ( 'NONE', #16769, #3293, #27611 ) ;
#7863=CIRCLE ( 'NONE', #20495, 9.499000000000000554 ) ;
#7913=EDGE_CURVE ( 'NONE', #22617, #22087, #5625, .T. ) ;
#7929=VECTOR ( 'NONE', #5027, 1000.000000000000000 ) ;
#7935=CIRCLE ( 'NONE', #17118, 4.800000000000001599 ) ;
#7938=ORIENTED_EDGE ( 'NONE', *, *, #6699, .F. ) ;
#7961=CARTESIAN_POINT ( 'NONE',  ( 0.000000000000000000, 0.000000000000000000, 0.000000000000000000 ) ) ;
#7974=AXIS2_PLACEMENT_3D ( 'NONE', #14647, #24950, #3354 ) ;
#7999=DIRECTION ( 'NONE',  ( 0.000000000000000000, 0.000000000000000000, 1.000000000000000000 ) ) ;
#8010=DIRECTION ( 'NONE',  ( -1.000000000000000000, 0.000000000000000000, 0.000000000000000000 ) ) ;
#8027=EDGE_LOOP ( 'NONE', ( #23701, #29739, #6628, #19444 ) ) ;
#8055=CARTESIAN_POINT ( 'NONE',  ( 0.000000000000000000, 0.000000000000000000, 0.000000000000000000 ) ) ;
#8077=EDGE_CURVE ( 'NONE', #10012, #20656, #19361, .T. ) ;
#8093=FACE_OUTER_BOUND ( 'NONE', #21092, .T. ) ;
#8099=DIRECTION ( 'NONE',  ( -1.000000000000000000, 0.000000000000000000, 0.000000000000000000 ) ) ;
#8123=DIRECTION ( 'NONE',  ( -1.000000000000000000, 0.000000000000000000, 0.000000000000000000 ) ) ;
#8128=CARTESIAN_POINT ( 'NONE',  ( 8.000000000000007105, -9.433698091065103597, 1.111908866155073117 ) ) ;
#8181=DIRECTION ( 'NONE',  ( 1.000000000000000000, -0.000000000000000000, 0.000000000000000000 ) ) ;
#8193=ORIENTED_EDGE ( 'NONE', *, *, #9856, .F. ) ;
#8232=DIRECTION ( 'NONE',  ( 0.000000000000000000, -0.8660254037844327124, -0.5000000000000104361 ) ) ;
#8242=ORIENTED_EDGE ( 'NONE', *, *, #24674, .T. ) ;
#8261=ORIENTED_EDGE ( 'NONE', *, *, #15867, .F. ) ;
#8279=ORIENTED_EDGE ( 'NONE', *, *, #6699, .T. ) ;
#8319=EDGE_LOOP ( 'NONE', ( #8356, #14772, #14837, #5605 ) ) ;
#8324=CLOSED_SHELL ( 'NONE', ( #1799, #15420, #31769, #33982, #29528, #14528, #24619, #31935, #27603, #13865, #31230, #20887, #16427, #13702, #19364, #14350, #11423, #21763, #22242, #21858, #23404, #20012, #23630, #5790, #7131, #26916, #4196, #31512, #26336, #33474, #31847, #24639, #16961, #11526, #22695, #12314, #19457, #30116, #26209, #5130, #14091, #1830, #5995, #6038, #13669, #22633, #34345, #23850, #10438, #19451, #2933, #3731, #11647, #14987, #2969, #7053, #16765, #18335, #3998, #104, #23820 ) ) ;
#8329=AXIS2_PLACEMENT_3D ( 'NONE', #29422, #4596, #6420 ) ;
#8356=ORIENTED_EDGE ( 'NONE', *, *, #24674, .F. ) ;
#8400=CARTESIAN_POINT ( 'NONE',  ( 8.000000000000007105, 3.268936481846368203, -13.61301047812914256 ) ) ;
#8401=EDGE_LOOP ( 'NONE', ( #19385, #30084, #29604, #9343 ) ) ;
#8409=VECTOR ( 'NONE', #8123, 1000.000000000000000 ) ;
#8416=DIRECTION ( 'NONE',  ( 1.000000000000000000, -0.000000000000000000, -0.000000000000000000 ) ) ;
#8439=VECTOR ( 'NONE', #24541, 1000.000000000000000 ) ;
#8454=DIRECTION ( 'NONE',  ( 0.000000000000000000, 0.000000000000000000, 1.000000000000000000 ) ) ;
#8471=CIRCLE ( 'NONE', #25134, 14.00000000000000000 ) ;
#8486=DIRECTION ( 'NONE',  ( -1.000000000000000000, 0.000000000000000000, 0.000000000000000000 ) ) ;
#8524=CARTESIAN_POINT ( 'NONE',  ( -9.999999999999994671, 0.000000000000000000, 0.000000000000000000 ) ) ;
#8529=DIRECTION ( 'NONE',  ( -1.000000000000000000, 0.000000000000000000, 0.000000000000000000 ) ) ;
#8535=CARTESIAN_POINT ( 'NONE',  ( 0.000000000000000000, -8.725776631572617958, -3.753907720749127819 ) ) ;
#8562=CARTESIAN_POINT ( 'NONE',  ( 0.000000000000000000, 0.000000000000000000, 0.000000000000000000 ) ) ;
#8586=DIRECTION ( 'NONE',  ( 0.000000000000000000, 0.4999999999999948375, 0.8660254037844415942 ) ) ;
#8625=EDGE_CURVE ( 'NONE', #13147, #25713, #5400, .T. ) ;
#8629=EDGE_CURVE ( 'NONE', #577, #27296, #11315, .T. ) ;
#8633=EDGE_CURVE ( 'NONE', #22893, #14025, #3227, .T. ) ;
#8642=AXIS2_PLACEMENT_3D ( 'NONE', #31209, #6017, #9418 ) ;
#8719=ORIENTED_EDGE ( 'NONE', *, *, #6638, .T. ) ;
#8734=LINE ( 'NONE', #640, #13616 ) ;
#8736=CARTESIAN_POINT ( 'NONE',  ( 8.000000000000007105, 9.604183132802452505, 5.908880290975567995 ) ) ;
#8746=ORIENTED_EDGE ( 'NONE', *, *, #30806, .T. ) ;
#8767=VECTOR ( 'NONE', #32807, 1000.000000000000000 ) ;
#8780=CARTESIAN_POINT ( 'NONE',  ( 8.000000000000007105, 9.433698091065215507, 1.111908866155128628 ) ) ;
#8794=CARTESIAN_POINT ( 'NONE',  ( 8.000000000000007105, 5.679790370316031733, 7.613867765417614564 ) ) ;
#8808=ORIENTED_EDGE ( 'NONE', *, *, #2029, .F. ) ;
#8813=AXIS2_PLACEMENT_3D ( 'NONE', #15349, #26361, #9966 ) ;
#8829=EDGE_CURVE ( 'NONE', #17787, #21028, #31292, .T. ) ;
#8833=DIRECTION ( 'NONE',  ( 0.000000000000000000, 0.000000000000000000, 1.000000000000000000 ) ) ;
#8845=AXIS2_PLACEMENT_3D ( 'NONE', #30562, #24812, #14337 ) ;
#8900=CYLINDRICAL_SURFACE ( 'NONE', #6252, 4.800000000000000711 ) ;
#8902=DIRECTION ( 'NONE',  ( 0.000000000000000000, 0.4999999999999948930, 0.8660254037844415942 ) ) ;
#8903=AXIS2_PLACEMENT_3D ( 'NONE', #14052, #5624, #28 ) ;
#8965=EDGE_CURVE ( 'NONE', #14457, #17480, #1588, .T. ) ;
#8984=DIRECTION ( 'NONE',  ( 0.000000000000000000, -1.000000000000000000, -1.049160758270772931E-14 ) ) ;
#8987=VERTEX_POINT ( 'NONE', #29131 ) ;
#9026=AXIS2_PLACEMENT_3D ( 'NONE', #26604, #18303, #32348 ) ;
#9095=DIRECTION ( 'NONE',  ( -1.000000000000000000, 0.000000000000000000, 0.000000000000000000 ) ) ;
#9133=CARTESIAN_POINT ( 'NONE',  ( 8.000000000000007105, 9.604183132802424083, -5.908880290975567995 ) ) ;
#9180=FACE_OUTER_BOUND ( 'NONE', #32829, .T. ) ;
#9193=ORIENTED_EDGE ( 'NONE', *, *, #22096, .T. ) ;
#9205=AXIS2_PLACEMENT_3D ( 'NONE', #16827, #28185, #11441 ) ;
#9207=EDGE_CURVE ( 'NONE', #12104, #24884, #4473, .T. ) ;
#9241=CARTESIAN_POINT ( 'NONE',  ( 8.000000000000007105, -5.679790370315976666, -7.613867765417642097 ) ) ;
#9250=DIRECTION ( 'NONE',  ( 1.000000000000000000, -0.000000000000000000, 0.000000000000000000 ) ) ;
#9251=ORIENTED_EDGE ( 'NONE', *, *, #1087, .T. ) ;
#9257=ORIENTED_EDGE ( 'NONE', *, *, #31533, .F. ) ;
#9258=EDGE_CURVE ( 'NONE', #17886, #15170, #23419, .T. ) ;
#9305=CIRCLE ( 'NONE', #9886, 4.800000000000000711 ) ;
#9342=EDGE_CURVE ( 'NONE', #15405, #17551, #13081, .T. ) ;
#9343=ORIENTED_EDGE ( 'NONE', *, *, #6858, .T. ) ;
#9385=AXIS2_PLACEMENT_3D ( 'NONE', #25595, #33162, #16589 ) ;
#9409=EDGE_CURVE ( 'NONE', #3677, #19516, #2808, .T. ) ;
#9418=DIRECTION ( 'NONE',  ( 0.000000000000000000, 0.8660254037844398178, -0.4999999999999977796 ) ) ;
#9457=CIRCLE ( 'NONE', #18086, 4.800000000000000711 ) ;
#9461=ORIENTED_EDGE ( 'NONE', *, *, #33761, .F. ) ;
#9467=CIRCLE ( 'NONE', #26734, 9.499000000000004107 ) ;
#9472=ORIENTED_EDGE ( 'NONE', *, *, #33761, .T. ) ;
#9475=AXIS2_PLACEMENT_3D ( 'NONE', #30104, #8486, #19106 ) ;
#9510=CARTESIAN_POINT ( 'NONE',  ( 0.000000000000000000, 0.000000000000000000, 0.000000000000000000 ) ) ;
#9516=DIRECTION ( 'NONE',  ( 0.000000000000000000, 0.5000000000000011102, -0.8660254037844379305 ) ) ;
#9557=VERTEX_POINT ( 'NONE', #1144 ) ;
#9569=ORIENTED_EDGE ( 'NONE', *, *, #26417, .F. ) ;
#9628=CYLINDRICAL_SURFACE ( 'NONE', #33364, 13.99999999999999822 ) ;
#9648=CIRCLE ( 'NONE', #13137, 4.800000000000000711 ) ;
#9664=EDGE_CURVE ( 'NONE', #18507, #25259, #31494, .T. ) ;
#9668=ORIENTED_EDGE ( 'NONE', *, *, #29137, .F. ) ;
#9673=EDGE_CURVE ( 'NONE', #21816, #31978, #29037, .T. ) ;
#9694=ORIENTED_EDGE ( 'NONE', *, *, #5891, .F. ) ;
#9696=DIRECTION ( 'NONE',  ( -1.000000000000000000, 0.000000000000000000, 0.000000000000000000 ) ) ;
#9710=ORIENTED_EDGE ( 'NONE', *, *, #22288, .T. ) ;
#9747=VERTEX_POINT ( 'NONE', #9949 ) ;
#9748=EDGE_CURVE ( 'NONE', #14694, #25713, #26335, .T. ) ;
#9775=EDGE_CURVE ( 'NONE', #21816, #34202, #10127, .T. ) ;
#9798=CARTESIAN_POINT ( 'NONE',  ( 8.000000000000007105, 0.3151488735050472778, -11.27190672109269087 ) ) ;
#9815=DIRECTION ( 'NONE',  ( 0.000000000000000000, 0.000000000000000000, 1.000000000000000000 ) ) ;
#9835=CARTESIAN_POINT ( 'NONE',  ( 8.000000000000007105, -1.111908866155017606, -9.433698091065132019 ) ) ;
#9846=CARTESIAN_POINT ( 'NONE',  ( 7.999999999999992895, 3.872983346207420574, -1.000000000000000888 ) ) ;
#9855=APPLICATION_CONTEXT ( 'automotive_design' ) ;
#9856=EDGE_CURVE ( 'NONE', #741, #26745, #19280, .T. ) ;
#9865=ORIENTED_EDGE ( 'NONE', *, *, #8633, .F. ) ;
#9886=AXIS2_PLACEMENT_3D ( 'NONE', #2359, #13500, #10619 ) ;
#9890=CARTESIAN_POINT ( 'NONE',  ( 8.000000000000007105, -3.975523202428068892, 13.42368113696675103 ) ) ;
#9900=CIRCLE ( 'NONE', #20230, 4.800000000000006928 ) ;
#9949=CARTESIAN_POINT ( 'NONE',  ( 8.000000000000007105, 9.433698091065215507, 1.111908866155128628 ) ) ;
#9962=EDGE_CURVE ( 'NONE', #20326, #24108, #35073, .T. ) ;
#9966=DIRECTION ( 'NONE',  ( 0.000000000000000000, 0.000000000000000000, 1.000000000000000000 ) ) ;
#9977=CARTESIAN_POINT ( 'NONE',  ( 0.000000000000000000, -9.604183132802312173, -5.908880290975638161 ) ) ;
#9991=EDGE_CURVE ( 'NONE', #10771, #4384, #17788, .T. ) ;
#9993=DIRECTION ( 'NONE',  ( -1.000000000000000000, 0.000000000000000000, 0.000000000000000000 ) ) ;
#9997=FACE_OUTER_BOUND ( 'NONE', #8401, .T. ) ;
#10012=VERTEX_POINT ( 'NONE', #6980 ) ;
#10017=LINE ( 'NONE', #9835, #32121 ) ;
#10020=ORIENTED_EDGE ( 'NONE', *, *, #24468, .F. ) ;
#10059=ORIENTED_EDGE ( 'NONE', *, *, #32301, .T. ) ;
#10064=CARTESIAN_POINT ( 'NONE',  ( 8.000000000000007105, 0.000000000000000000, 0.000000000000000000 ) ) ;
#10068=AXIS2_PLACEMENT_3D ( 'NONE', #21984, #16585, #32981 ) ;
#10083=AXIS2_PLACEMENT_3D ( 'NONE', #12525, #1192, #9815 ) ;
#10094=VERTEX_POINT ( 'NONE', #22685 ) ;
#10098=DIRECTION ( 'NONE',  ( 0.000000000000000000, 0.8660254037844362651, 0.5000000000000042188 ) ) ;
#10113=DIRECTION ( 'NONE',  ( -1.000000000000000000, 0.000000000000000000, 0.000000000000000000 ) ) ;
#10127=LINE ( 'NONE', #21093, #14231 ) ;
#10131=DIRECTION ( 'NONE',  ( -1.000000000000000000, 0.000000000000000000, 0.000000000000000000 ) ) ;
#10148=( LENGTH_UNIT ( ) NAMED_UNIT ( * ) SI_UNIT ( .MILLI., .METRE. ) );
#10162=DIRECTION ( 'NONE',  ( -1.000000000000000000, 0.000000000000000000, 0.000000000000000000 ) ) ;
#10187=FACE_OUTER_BOUND ( 'NONE', #30304, .T. ) ;
#10212=DIRECTION ( 'NONE',  ( -1.000000000000000000, 0.000000000000000000, 0.000000000000000000 ) ) ;
#10227=VECTOR ( 'NONE', #13655, 1000.000000000000000 ) ;
#10248=DIRECTION ( 'NONE',  ( 0.000000000000000000, -0.5000000000000067724, 0.8660254037844348218 ) ) ;
#10283=VECTOR ( 'NONE', #14649, 1000.000000000000000 ) ;
#10286=CARTESIAN_POINT ( 'NONE',  ( 0.000000000000000000, -1.111908866155156161, 9.433698091065117808 ) ) ;
#10292=ORIENTED_EDGE ( 'NONE', *, *, #16558, .F. ) ;
#10328=AXIS2_PLACEMENT_3D ( 'NONE', #6881, #10113, #12464 ) ;
#10338=ORIENTED_EDGE ( 'NONE', *, *, #18882, .T. ) ;
#10346=VECTOR ( 'NONE', #25133, 1000.000000000000000 ) ;
#10389=DIRECTION ( 'NONE',  ( 0.000000000000000000, 0.000000000000000000, 1.000000000000000000 ) ) ;
#10415=AXIS2_PLACEMENT_3D ( 'NONE', #2560, #7751, #4900 ) ;
#10423=ORIENTED_EDGE ( 'NONE', *, *, #2477, .F. ) ;
#10424=VERTEX_POINT ( 'NONE', #31432 ) ;
#10431=EDGE_LOOP ( 'NONE', ( #28570, #31808, #12123, #28379 ) ) ;
#10438=ADVANCED_FACE ( 'NONE', ( #31253 ), #6576, .T. ) ;
#10458=CARTESIAN_POINT ( 'NONE',  ( 8.000000000000007105, -8.725776631572701447, 3.753907720749016796 ) ) ;
#10473=VERTEX_POINT ( 'NONE', #20418 ) ;
#10482=VECTOR ( 'NONE', #10212, 1000.000000000000000 ) ;
#10492=VECTOR ( 'NONE', #8529, 1000.000000000000000 ) ;
#10498=ORIENTED_EDGE ( 'NONE', *, *, #7460, .T. ) ;
#10532=EDGE_LOOP ( 'NONE', ( #29913, #6332, #7051, #29253 ) ) ;
#10556=AXIS2_PLACEMENT_3D ( 'NONE', #34532, #3944, #25722 ) ;
#10566=AXIS2_PLACEMENT_3D ( 'NONE', #20103, #31110, #6438 ) ;
#10568=DIRECTION ( 'NONE',  ( 0.000000000000000000, 0.000000000000000000, 1.000000000000000000 ) ) ;
#10590=CARTESIAN_POINT ( 'NONE',  ( 8.000000000000007105, 1.111908866155100650, 9.433698091065117808 ) ) ;
#10600=ORIENTED_EDGE ( 'NONE', *, *, #15820, .F. ) ;
#10619=DIRECTION ( 'NONE',  ( 0.000000000000000000, 0.000000000000000000, -1.000000000000000000 ) ) ;
#10632=CYLINDRICAL_SURFACE ( 'NONE', #13099, 4.800000000000000711 ) ;
#10643=VERTEX_POINT ( 'NONE', #28911 ) ;
#10644=FACE_OUTER_BOUND ( 'NONE', #32113, .T. ) ;
#10684=VERTEX_POINT ( 'NONE', #8535 ) ;
#10692=CARTESIAN_POINT ( 'NONE',  ( 0.000000000000000000, -3.753907720748892007, -8.725776631572756514 ) ) ;
#10706=DIRECTION ( 'NONE',  ( -1.000000000000000000, 0.000000000000000000, 0.000000000000000000 ) ) ;
#10722=EDGE_CURVE ( 'NONE', #24884, #16008, #5844, .T. ) ;
#10724=CARTESIAN_POINT ( 'NONE',  ( 8.000000000000007105, 3.753907720749127819, 8.725776631572756514 ) ) ;
#10733=AXIS2_PLACEMENT_3D ( 'NONE', #12260, #25783, #8833 ) ;
#10737=DIRECTION ( 'NONE',  ( -1.000000000000000000, 0.000000000000000000, 0.000000000000000000 ) ) ;
#10745=CIRCLE ( 'NONE', #7851, 4.800000000000006040 ) ;
#10748=CARTESIAN_POINT ( 'NONE',  ( 4.000000000000003553, -13.42368113696662490, -3.975523202428152381 ) ) ;
#10754=CARTESIAN_POINT ( 'NONE',  ( 8.000000000000007105, -1.111908866155156161, 9.433698091065117808 ) ) ;
#10771=VERTEX_POINT ( 'NONE', #5325 ) ;
#10796=CARTESIAN_POINT ( 'NONE',  ( 0.000000000000000000, 1.111908866155322695, -9.433698091065103597 ) ) ;
#10828=CARTESIAN_POINT ( 'NONE',  ( 8.000000000000007105, 1.111908866155322695, -9.433698091065103597 ) ) ;
#10834=VERTEX_POINT ( 'NONE', #7825 ) ;
#10837=ORIENTED_EDGE ( 'NONE', *, *, #22288, .F. ) ;
#10867=ORIENTED_EDGE ( 'NONE', *, *, #24743, .F. ) ;
#10900=DIRECTION ( 'NONE',  ( -1.000000000000000000, 0.000000000000000000, 0.000000000000000000 ) ) ;
#10945=VECTOR ( 'NONE', #26297, 1000.000000000000000 ) ;
#10954=DIRECTION ( 'NONE',  ( -1.000000000000000000, 0.000000000000000000, 0.000000000000000000 ) ) ;
#10988=DIRECTION ( 'NONE',  ( 0.000000000000000000, -0.4999999999999891753, -0.8660254037844450359 ) ) ;
#10996=AXIS2_PLACEMENT_3D ( 'NONE', #19736, #22990, #17226 ) ;
#10998=EDGE_CURVE ( 'NONE', #6287, #21466, #24185, .T. ) ;
#11018=CYLINDRICAL_SURFACE ( 'NONE', #8903, 4.800000000000000711 ) ;
#11025=AXIS2_PLACEMENT_3D ( 'NONE', #13996, #8416, #33271 ) ;
#11028=ORIENTED_EDGE ( 'NONE', *, *, #5891, .T. ) ;
#11035=FACE_OUTER_BOUND ( 'NONE', #14920, .T. ) ;
#11063=EDGE_LOOP ( 'NONE', ( #669, #34277, #32430, #6604 ) ) ;
#11107=CARTESIAN_POINT ( 'NONE',  ( 8.000000000000007105, 11.27190672109271219, 0.3151488735049640111 ) ) ;
#11111=DIRECTION ( 'NONE',  ( -1.000000000000000000, 0.000000000000000000, 0.000000000000000000 ) ) ;
#11125=EDGE_LOOP ( 'NONE', ( #22611, #18583, #26906, #3197 ) ) ;
#11139=CARTESIAN_POINT ( 'NONE',  ( 8.000000000000007105, -9.604183132802312173, -5.908880290975638161 ) ) ;
#11147=DIRECTION ( 'NONE',  ( 1.000000000000000000, -0.000000000000000000, -0.000000000000000000 ) ) ;
#11154=ORIENTED_EDGE ( 'NONE', *, *, #1002, .F. ) ;
#11159=LINE ( 'NONE', #35313, #15942 ) ;
#11176=CARTESIAN_POINT ( 'NONE',  ( 0.000000000000000000, 0.000000000000000000, 0.000000000000000000 ) ) ;
#11195=DIRECTION ( 'NONE',  ( -1.000000000000000000, 0.000000000000000000, 0.000000000000000000 ) ) ;
#11213=DIRECTION ( 'NONE',  ( 0.000000000000000000, 0.8660254037844398178, -0.4999999999999977796 ) ) ;
#11246=ORIENTED_EDGE ( 'NONE', *, *, #28248, .T. ) ;
#11262=DIRECTION ( 'NONE',  ( -1.000000000000000000, 0.000000000000000000, 0.000000000000000000 ) ) ;
#11289=FACE_OUTER_BOUND ( 'NONE', #23835, .T. ) ;
#11291=ORIENTED_EDGE ( 'NONE', *, *, #9207, .T. ) ;
#11313=ORIENTED_EDGE ( 'NONE', *, *, #9962, .F. ) ;
#11315=CIRCLE ( 'NONE', #5595, 9.499000000000009436 ) ;
#11332=AXIS2_PLACEMENT_3D ( 'NONE', #21373, #30032, #2853 ) ;
#11340=ORIENTED_EDGE ( 'NONE', *, *, #32353, .F. ) ;
#11351=CARTESIAN_POINT ( 'NONE',  ( 4.000000000000003553, -3.975523202427916125, -13.42368113696675636 ) ) ;
#11385=DIRECTION ( 'NONE',  ( -1.000000000000000000, 0.000000000000000000, 0.000000000000000000 ) ) ;
#11423=ADVANCED_FACE ( 'NONE', ( #3817 ), #923, .T. ) ;
#11437=DIRECTION ( 'NONE',  ( -1.000000000000000000, 0.000000000000000000, 0.000000000000000000 ) ) ;
#11441=DIRECTION ( 'NONE',  ( 0.000000000000000000, 0.000000000000000000, 1.000000000000000000 ) ) ;
#11509=ORIENTED_EDGE ( 'NONE', *, *, #2075, .F. ) ;
#11526=ADVANCED_FACE ( 'NONE', ( #4354 ), #31697, .T. ) ;
#11558=ORIENTED_EDGE ( 'NONE', *, *, #8625, .F. ) ;
#11578=STYLED_ITEM ( 'NONE', ( #16606 ), #29257 ) ;
#11583=DIRECTION ( 'NONE',  ( -1.000000000000000000, 0.000000000000000000, 0.000000000000000000 ) ) ;
#11589=DIRECTION ( 'NONE',  ( 0.000000000000000000, 0.000000000000000000, 1.000000000000000000 ) ) ;
#11606=LINE ( 'NONE', #3699, #10283 ) ;
#11623=VERTEX_POINT ( 'NONE', #23602 ) ;
#11630=AXIS2_PLACEMENT_3D ( 'NONE', #26568, #4253, #29268 ) ;
#11636=EDGE_CURVE ( 'NONE', #7004, #17434, #4004, .T. ) ;
#11645=ORIENTED_EDGE ( 'NONE', *, *, #35025, .F. ) ;
#11647=ADVANCED_FACE ( 'NONE', ( #12265 ), #23239, .T. ) ;
#11651=EDGE_CURVE ( 'NONE', #16526, #620, #3572, .T. ) ;
#11686=EDGE_CURVE ( 'NONE', #24324, #5109, #6434, .T. ) ;
#11690=ORIENTED_EDGE ( 'NONE', *, *, #20938, .F. ) ;
#11691=ORIENTED_EDGE ( 'NONE', *, *, #23117, .T. ) ;
#11694=CIRCLE ( 'NONE', #30113, 9.499000000000000554 ) ;
#11699=EDGE_CURVE ( 'NONE', #32057, #9747, #17294, .T. ) ;
#11733=SHAPE_REPRESENTATION_RELATIONSHIP ( 'NONE' , 'NONE' ,  #22901, #29257 ) ;
#11742=AXIS2_PLACEMENT_3D ( 'NONE', #17603, #9696, #18145 ) ;
#11756=EDGE_CURVE ( 'NONE', #3873, #22893, #21905, .T. ) ;
#11800=EDGE_CURVE ( 'NONE', #35157, #24108, #15569, .T. ) ;
#11832=DIRECTION ( 'NONE',  ( -1.000000000000000000, 0.000000000000000000, 0.000000000000000000 ) ) ;
#11835=CARTESIAN_POINT ( 'NONE',  ( 50.00005079999998969, 9.714451465470119729E-14, 1.000000000000000888 ) ) ;
#11850=CARTESIAN_POINT ( 'NONE',  ( 8.000000000000007105, 11.27190672109280811, -0.3151488735047974776 ) ) ;
#11925=ORIENTED_EDGE ( 'NONE', *, *, #1450, .F. ) ;
#11950=DIRECTION ( 'NONE',  ( -1.000000000000000000, 0.000000000000000000, 0.000000000000000000 ) ) ;
#11993=CARTESIAN_POINT ( 'NONE',  ( 0.000000000000000000, 11.27190672109271219, 0.3151488735049640111 ) ) ;
#12041=FACE_OUTER_BOUND ( 'NONE', #5264, .T. ) ;
#12099=CARTESIAN_POINT ( 'NONE',  ( 8.000000000000007105, 8.725776631572825792, 3.753907720749072308 ) ) ;
#12104=VERTEX_POINT ( 'NONE', #16200 ) ;
#12123=ORIENTED_EDGE ( 'NONE', *, *, #17374, .T. ) ;
#12153=EDGE_CURVE ( 'NONE', #11623, #20005, #21928, .T. ) ;
#12183=ORIENTED_EDGE ( 'NONE', *, *, #25579, .F. ) ;
#12206=FACE_OUTER_BOUND ( 'NONE', #23888, .T. ) ;
#12239=DIRECTION ( 'NONE',  ( 0.000000000000000000, -0.5000000000000067724, 0.8660254037844348218 ) ) ;
#12240=LINE ( 'NONE', #3977, #31013 ) ;
#12245=VECTOR ( 'NONE', #17987, 1000.000000000000000 ) ;
#12257=ORIENTED_EDGE ( 'NONE', *, *, #17786, .T. ) ;
#12260=CARTESIAN_POINT ( 'NONE',  ( 8.000000000000007105, 9.919332006307222116, 5.363026430117163734 ) ) ;
#12265=FACE_OUTER_BOUND ( 'NONE', #6069, .T. ) ;
#12266=DIRECTION ( 'NONE',  ( 0.000000000000000000, -0.4999999999999891753, -0.8660254037844450359 ) ) ;
#12293=CIRCLE ( 'NONE', #16307, 14.00000000000000000 ) ;
#12296=DIRECTION ( 'NONE',  ( 0.000000000000000000, 0.000000000000000000, 1.000000000000000000 ) ) ;
#12299=CARTESIAN_POINT ( 'NONE',  ( 8.000000000000007105, -10.15474465512046542, 9.637487275701101197 ) ) ;
#12314=ADVANCED_FACE ( 'NONE', ( #3740 ), #15406, .T. ) ;
#12323=DIRECTION ( 'NONE',  ( -1.000000000000000000, 0.000000000000000000, 0.000000000000000000 ) ) ;
#12344=EDGE_CURVE ( 'NONE', #21924, #35157, #15758, .T. ) ;
#12373=CYLINDRICAL_SURFACE ( 'NONE', #24789, 13.99999999999999822 ) ;
#12395=PRODUCT ( 'spur gear_iso_ISO - Spur gear 2M 12T 20PA 8FW ---S12A75H50L8.0S1', 'spur gear_iso_ISO - Spur gear 2M 12T 20PA 8FW ---S12A75H50L8.0S1', '', ( #14689 ) ) ;
#12399=ORIENTED_EDGE ( 'NONE', *, *, #22440, .T. ) ;
#12406=DIRECTION ( 'NONE',  ( 0.000000000000000000, 0.000000000000000000, 1.000000000000000000 ) ) ;
#12416=EDGE_CURVE ( 'NONE', #25674, #7004, #18511, .T. ) ;
#12444=ORIENTED_EDGE ( 'NONE', *, *, #22765, .T. ) ;
#12455=ORIENTED_EDGE ( 'NONE', *, *, #544, .F. ) ;
#12464=DIRECTION ( 'NONE',  ( 0.000000000000000000, 0.5000000000000011102, -0.8660254037844380415 ) ) ;
#12481=CIRCLE ( 'NONE', #16470, 4.800000000000006040 ) ;
#12483=VECTOR ( 'NONE', #34815, 1000.000000000000000 ) ;
#12490=ORIENTED_EDGE ( 'NONE', *, *, #14695, .F. ) ;
#12499=ORIENTED_EDGE ( 'NONE', *, *, #6635, .T. ) ;
#12514=UNCERTAINTY_MEASURE_WITH_UNIT (LENGTH_MEASURE( 1.000000000000000082E-05 ), #1096, 'distance_accuracy_value', 'NONE');
#12525=CARTESIAN_POINT ( 'NONE',  ( 8.000000000000007105, 0.000000000000000000, 0.000000000000000000 ) ) ;
#12535=ORIENTED_EDGE ( 'NONE', *, *, #5088, .F. ) ;
#12537=AXIS2_PLACEMENT_3D ( 'NONE', #20836, #25309, #8586 ) ;
#12555=EDGE_CURVE ( 'NONE', #25713, #28225, #2914, .T. ) ;
#12585=ORIENTED_EDGE ( 'NONE', *, *, #7577, .T. ) ;
#12595=ORIENTED_EDGE ( 'NONE', *, *, #478, .F. ) ;
#12611=EDGE_CURVE ( 'NONE', #1909, #23255, #12788, .T. ) ;
#12613=SURFACE_SIDE_STYLE ('',( #18174 ) ) ;
#12633=CARTESIAN_POINT ( 'NONE',  ( 0.000000000000000000, 10.15474465512070168, -9.637487275700989287 ) ) ;
#12638=CARTESIAN_POINT ( 'NONE',  ( 0.000000000000000000, 7.613867765417669631, 5.679790370316101011 ) ) ;
#12664=CARTESIAN_POINT ( 'NONE',  ( 8.000000000000007105, -13.61301047812919762, 3.268936481846118625 ) ) ;
#12694=CIRCLE ( 'NONE', #10415, 4.800000000000000711 ) ;
#12725=DIRECTION ( 'NONE',  ( 0.000000000000000000, 0.000000000000000000, 1.000000000000000000 ) ) ;
#12735=CARTESIAN_POINT ( 'NONE',  ( 0.000000000000000000, -3.975523202428068892, 13.42368113696675103 ) ) ;
#12765=CARTESIAN_POINT ( 'NONE',  ( 8.000000000000007105, 3.268936481846187903, 13.61301047812924025 ) ) ;
#12788=LINE ( 'NONE', #2189, #10945 ) ;
#12806=DIRECTION ( 'NONE',  ( -1.000000000000000000, 0.000000000000000000, 0.000000000000000000 ) ) ;
#12843=DIRECTION ( 'NONE',  ( 0.000000000000000000, -1.000000000000000000, 0.000000000000000000 ) ) ;
#12863=EDGE_LOOP ( 'NONE', ( #14955, #13094, #5010, #35068 ) ) ;
#12878=EDGE_LOOP ( 'NONE', ( #10059, #3516, #13506, #4007 ) ) ;
#12968=EDGE_LOOP ( 'NONE', ( #8261, #32240, #1558, #27942 ) ) ;
#12970=CARTESIAN_POINT ( 'NONE',  ( 4.000000000000003553, 13.42368113696688958, -3.975523202427861058 ) ) ;
#12971=CIRCLE ( 'NONE', #14659, 4.800000000000006040 ) ;
#12980=ORIENTED_EDGE ( 'NONE', *, *, #31983, .F. ) ;
#13020=CARTESIAN_POINT ( 'NONE',  ( 8.000000000000007105, -5.679790370316031733, 7.613867765417587030 ) ) ;
#13050=LINE ( 'NONE', #13230, #1300 ) ;
#13056=DIRECTION ( 'NONE',  ( 0.000000000000000000, 0.000000000000000000, 1.000000000000000000 ) ) ;
#13069=CARTESIAN_POINT ( 'NONE',  ( 4.000000000000003553, 13.42368113696682030, 3.975523202428055125 ) ) ;
#13081=CIRCLE ( 'NONE', #26883, 4.800000000000006040 ) ;
#13091=CIRCLE ( 'NONE', #22820, 9.499000000000012989 ) ;
#13094=ORIENTED_EDGE ( 'NONE', *, *, #20227, .F. ) ;
#13099=AXIS2_PLACEMENT_3D ( 'NONE', #5068, #34636, #8454 ) ;
#13100=DIRECTION ( 'NONE',  ( 0.000000000000000000, 0.000000000000000000, 1.000000000000000000 ) ) ;
#13133=ORIENTED_EDGE ( 'NONE', *, *, #29426, .F. ) ;
#13137=AXIS2_PLACEMENT_3D ( 'NONE', #34034, #34212, #17806 ) ;
#13147=VERTEX_POINT ( 'NONE', #34713 ) ;
#13154=CARTESIAN_POINT ( 'NONE',  ( 8.000000000000007105, 9.919332006307387317, -5.363026430117004750 ) ) ;
#13159=EDGE_LOOP ( 'NONE', ( #15273, #2919, #13386, #2782 ) ) ;
#13172=CARTESIAN_POINT ( 'NONE',  ( 0.000000000000000000, 0.000000000000000000, 0.000000000000000000 ) ) ;
#13227=EDGE_CURVE ( 'NONE', #33344, #18371, #18430, .T. ) ;
#13228=DIRECTION ( 'NONE',  ( 0.000000000000000000, 0.000000000000000000, 1.000000000000000000 ) ) ;
#13230=CARTESIAN_POINT ( 'NONE',  ( 4.000000000000003553, 3.975523202428290936, -13.42368113696666754 ) ) ;
#13242=DIRECTION ( 'NONE',  ( -1.000000000000000000, 0.000000000000000000, 0.000000000000000000 ) ) ;
#13248=VERTEX_POINT ( 'NONE', #30193 ) ;
#13272=VECTOR ( 'NONE', #27471, 1000.000000000000000 ) ;
#13290=EDGE_CURVE ( 'NONE', #10684, #11623, #23986, .T. ) ;
#13312=VERTEX_POINT ( 'NONE', #19369 ) ;
#13332=DIRECTION ( 'NONE',  ( 1.000000000000000000, -0.000000000000000000, -0.000000000000000000 ) ) ;
#13361=CARTESIAN_POINT ( 'NONE',  ( 8.000000000000007105, 10.15474465512060398, 9.637487275701170475 ) ) ;
#13373=ORIENTED_EDGE ( 'NONE', *, *, #15157, .F. ) ;
#13381=DIRECTION ( 'NONE',  ( -1.000000000000000000, 0.000000000000000000, 0.000000000000000000 ) ) ;
#13386=ORIENTED_EDGE ( 'NONE', *, *, #27591, .T. ) ;
#13413=CARTESIAN_POINT ( 'NONE',  ( 4.000000000000003553, 9.637487275701349887, -10.15474465512039615 ) ) ;
#13450=EDGE_CURVE ( 'NONE', #6425, #29329, #14169, .T. ) ;
#13452=EDGE_CURVE ( 'NONE', #20326, #10473, #17605, .T. ) ;
#13462=EDGE_CURVE ( 'NONE', #29830, #26423, #8734, .T. ) ;
#13492=CARTESIAN_POINT ( 'NONE',  ( 0.000000000000000000, 0.000000000000000000, 0.000000000000000000 ) ) ;
#13500=DIRECTION ( 'NONE',  ( 1.000000000000000000, -0.000000000000000000, 0.000000000000000000 ) ) ;
#13506=ORIENTED_EDGE ( 'NONE', *, *, #27117, .F. ) ;
#13565=ORIENTED_EDGE ( 'NONE', *, *, #5046, .T. ) ;
#13569=EDGE_CURVE ( 'NONE', #33265, #13312, #15193, .T. ) ;
#13589=CARTESIAN_POINT ( 'NONE',  ( 0.000000000000000000, -9.604183132802312173, -1.108880290975637228 ) ) ;
#13590=CARTESIAN_POINT ( 'NONE',  ( 0.000000000000000000, 3.753907720749127819, 8.725776631572756514 ) ) ;
#13616=VECTOR ( 'NONE', #20414, 1000.000000000000000 ) ;
#13635=CIRCLE ( 'NONE', #16497, 4.800000000000000711 ) ;
#13655=DIRECTION ( 'NONE',  ( 1.000000000000000000, -0.000000000000000000, -0.000000000000000000 ) ) ;
#13669=ADVANCED_FACE ( 'NONE', ( #21145 ), #18448, .T. ) ;
#13675=DIRECTION ( 'NONE',  ( -1.000000000000000000, 0.000000000000000000, 0.000000000000000000 ) ) ;
#13702=ADVANCED_FACE ( 'NONE', ( #30152 ), #19155, .T. ) ;
#13739=CARTESIAN_POINT ( 'NONE',  ( 8.000000000000007105, -5.908880290975582206, 9.604183132802395662 ) ) ;
#13826=DIRECTION ( 'NONE',  ( -1.000000000000000000, 0.000000000000000000, 0.000000000000000000 ) ) ;
#13863=ORIENTED_EDGE ( 'NONE', *, *, #1002, .T. ) ;
#13865=ADVANCED_FACE ( 'NONE', ( #34912 ), #16139, .F. ) ;
#13887=DIRECTION ( 'NONE',  ( 0.000000000000000000, 0.000000000000000000, 1.000000000000000000 ) ) ;
#13890=EDGE_CURVE ( 'NONE', #21924, #10834, #23402, .T. ) ;
#13896=DIRECTION ( 'NONE',  ( -1.000000000000000000, 0.000000000000000000, 0.000000000000000000 ) ) ;
#13903=EDGE_CURVE ( 'NONE', #29830, #20425, #8471, .T. ) ;
#13930=CYLINDRICAL_SURFACE ( 'NONE', #5520, 13.99999999999999822 ) ;
#13957=VERTEX_POINT ( 'NONE', #5540 ) ;
#13962=EDGE_CURVE ( 'NONE', #10094, #33676, #17632, .T. ) ;
#13996=CARTESIAN_POINT ( 'NONE',  ( 7.999999999999992895, 0.000000000000000000, 0.000000000000000000 ) ) ;
#13997=ORIENTED_EDGE ( 'NONE', *, *, #4931, .F. ) ;
#14012=CARTESIAN_POINT ( 'NONE',  ( 4.000000000000003553, 3.268936481846368203, -13.61301047812914256 ) ) ;
#14025=VERTEX_POINT ( 'NONE', #8400 ) ;
#14052=CARTESIAN_POINT ( 'NONE',  ( 8.000000000000007105, 5.363026430117337817, -9.919332006307165273 ) ) ;
#14062=ORIENTED_EDGE ( 'NONE', *, *, #9258, .T. ) ;
#14068=CIRCLE ( 'NONE', #10068, 13.99999999999999645 ) ;
#14075=( NAMED_UNIT ( * ) PLANE_ANGLE_UNIT ( ) SI_UNIT ( $, .RADIAN. ) );
#14077=VERTEX_POINT ( 'NONE', #17023 ) ;
#14091=ADVANCED_FACE ( 'NONE', ( #11289 ), #33423, .T. ) ;
#14149=EDGE_LOOP ( 'NONE', ( #3826, #35191, #32996, #21412 ) ) ;
#14165=CIRCLE ( 'NONE', #362, 4.800000000000002487 ) ;
#14169=CIRCLE ( 'NONE', #20478, 14.00000000000000000 ) ;
#14174=FACE_OUTER_BOUND ( 'NONE', #31907, .T. ) ;
#14178=LINE ( 'NONE', #22986, #16272 ) ;
#14183=DIRECTION ( 'NONE',  ( -1.000000000000000000, 0.000000000000000000, 0.000000000000000000 ) ) ;
#14231=VECTOR ( 'NONE', #2934, 1000.000000000000000 ) ;
#14261=FACE_OUTER_BOUND ( 'NONE', #8319, .T. ) ;
#14263=FACE_OUTER_BOUND ( 'NONE', #31143, .T. ) ;
#14278=ORIENTED_EDGE ( 'NONE', *, *, #15678, .F. ) ;
#14289=ORIENTED_EDGE ( 'NONE', *, *, #20938, .T. ) ;
#14306=CARTESIAN_POINT ( 'NONE',  ( 0.000000000000000000, 9.714451465470119729E-14, 1.000000000000000888 ) ) ;
#14322=ORIENTED_EDGE ( 'NONE', *, *, #13290, .F. ) ;
#14328=DIRECTION ( 'NONE',  ( 0.000000000000000000, 0.000000000000000000, 1.000000000000000000 ) ) ;
#14333=ORIENTED_EDGE ( 'NONE', *, *, #21512, .T. ) ;
#14337=DIRECTION ( 'NONE',  ( 0.000000000000000000, 0.000000000000000000, 1.000000000000000000 ) ) ;
#14343=DIRECTION ( 'NONE',  ( 0.000000000000000000, 0.000000000000000000, 1.000000000000000000 ) ) ;
#14346=DIRECTION ( 'NONE',  ( -1.000000000000000000, 0.000000000000000000, 0.000000000000000000 ) ) ;
#14350=ADVANCED_FACE ( 'NONE', ( #10187 ), #27287, .T. ) ;
#14406=ORIENTED_EDGE ( 'NONE', *, *, #13452, .T. ) ;
#14409=DIRECTION ( 'NONE',  ( -1.000000000000000000, 0.000000000000000000, 0.000000000000000000 ) ) ;
#14425=VERTEX_POINT ( 'NONE', #16094 ) ;
#14457=VERTEX_POINT ( 'NONE', #26944 ) ;
#14471=CYLINDRICAL_SURFACE ( 'NONE', #7974, 13.99999999999999822 ) ;
#14494=CARTESIAN_POINT ( 'NONE',  ( 0.000000000000000000, 11.27190672109280811, 4.484851126495202678 ) ) ;
#14513=CYLINDRICAL_SURFACE ( 'NONE', #22592, 4.800000000000000711 ) ;
#14519=CARTESIAN_POINT ( 'NONE',  ( 8.000000000000007105, -11.27190672109260028, 4.484851126495120077 ) ) ;
#14528=ADVANCED_FACE ( 'NONE', ( #30162 ), #89, .F. ) ;
#14538=FACE_OUTER_BOUND ( 'NONE', #18536, .T. ) ;
#14558=AXIS2_PLACEMENT_3D ( 'NONE', #18721, #30076, #5417 ) ;
#14647=CARTESIAN_POINT ( 'NONE',  ( -9.999999999999994671, 0.000000000000000000, 0.000000000000000000 ) ) ;
#14649=DIRECTION ( 'NONE',  ( 1.000000000000000000, -0.000000000000000000, -0.000000000000000000 ) ) ;
#14653=LINE ( 'NONE', #14306, #10346 ) ;
#14659=AXIS2_PLACEMENT_3D ( 'NONE', #17192, #23138, #6758 ) ;
#14685=CYLINDRICAL_SURFACE ( 'NONE', #8329, 4.800000000000000711 ) ;
#14689=PRODUCT_CONTEXT ( 'NONE', #9855, 'mechanical' ) ;
#14692=CARTESIAN_POINT ( 'NONE',  ( 8.000000000000007105, 0.000000000000000000, 0.000000000000000000 ) ) ;
#14694=VERTEX_POINT ( 'NONE', #28702 ) ;
#14695=EDGE_CURVE ( 'NONE', #16232, #25092, #15882, .T. ) ;
#14697=CARTESIAN_POINT ( 'NONE',  ( 8.000000000000007105, 5.908880290975762506, -9.604183132802354805 ) ) ;
#14698=FACE_OUTER_BOUND ( 'NONE', #4964, .T. ) ;
#14702=VECTOR ( 'NONE', #19746, 1000.000000000000000 ) ;
#14704=DIRECTION ( 'NONE',  ( -1.000000000000000000, 0.000000000000000000, 0.000000000000000000 ) ) ;
#14728=DIRECTION ( 'NONE',  ( 0.000000000000000000, 0.000000000000000000, 1.000000000000000000 ) ) ;
#14771=FACE_OUTER_BOUND ( 'NONE', #25432, .T. ) ;
#14772=ORIENTED_EDGE ( 'NONE', *, *, #24670, .F. ) ;
#14784=LINE ( 'NONE', #25793, #16511 ) ;
#14810=DIRECTION ( 'NONE',  ( 0.000000000000000000, 1.000000000000000000, 3.614007241618346010E-15 ) ) ;
#14816=LINE ( 'NONE', #25094, #10492 ) ;
#14837=ORIENTED_EDGE ( 'NONE', *, *, #9409, .F. ) ;
#14860=DIRECTION ( 'NONE',  ( -1.000000000000000000, 0.000000000000000000, 0.000000000000000000 ) ) ;
#14920=EDGE_LOOP ( 'NONE', ( #8242, #21557, #12499, #12399 ) ) ;
#14923=EDGE_CURVE ( 'NONE', #577, #16232, #34639, .T. ) ;
#14933=CARTESIAN_POINT ( 'NONE',  ( -9.999999999999994671, 0.000000000000000000, 0.000000000000000000 ) ) ;
#14950=ORIENTED_EDGE ( 'NONE', *, *, #33524, .T. ) ;
#14955=ORIENTED_EDGE ( 'NONE', *, *, #13462, .T. ) ;
#14977=UNCERTAINTY_MEASURE_WITH_UNIT (LENGTH_MEASURE( 1.000000000000000082E-05 ), #27787, 'distance_accuracy_value', 'NONE');
#14978=DIRECTION ( 'NONE',  ( 0.000000000000000000, 0.000000000000000000, 1.000000000000000000 ) ) ;
#14980=EDGE_CURVE ( 'NONE', #18383, #23680, #2155, .T. ) ;
#14986=CARTESIAN_POINT ( 'NONE',  ( 8.000000000000007105, -9.433698091065103597, 1.111908866155073117 ) ) ;
#14987=ADVANCED_FACE ( 'NONE', ( #11035 ), #21997, .T. ) ;
#14999=ORIENTED_EDGE ( 'NONE', *, *, #13890, .F. ) ;
#15008=AXIS2_PLACEMENT_3D ( 'NONE', #4178, #1649, #1461 ) ;
#15051=DIRECTION ( 'NONE',  ( -1.000000000000000000, 0.000000000000000000, 0.000000000000000000 ) ) ;
#15066=LINE ( 'NONE', #8780, #14702 ) ;
#15080=AXIS2_PLACEMENT_3D ( 'NONE', #20941, #4947, #31760 ) ;
#15114=ORIENTED_EDGE ( 'NONE', *, *, #11699, .T. ) ;
#15155=DIRECTION ( 'NONE',  ( -1.000000000000000000, 0.000000000000000000, 0.000000000000000000 ) ) ;
#15157=EDGE_CURVE ( 'NONE', #16196, #6246, #6153, .T. ) ;
#15170=VERTEX_POINT ( 'NONE', #30652 ) ;
#15177=AXIS2_PLACEMENT_3D ( 'NONE', #31130, #23198, #28613 ) ;
#15183=DIRECTION ( 'NONE',  ( -1.000000000000000000, 0.000000000000000000, 0.000000000000000000 ) ) ;
#15193=LINE ( 'NONE', #13069, #35504 ) ;
#15207=EDGE_LOOP ( 'NONE', ( #18825, #34229, #17282, #5451 ) ) ;
#15217=CARTESIAN_POINT ( 'NONE',  ( 0.000000000000000000, 4.898587196589412829E-16, -4.000000000000000000 ) ) ;
#15241=DIRECTION ( 'NONE',  ( 0.000000000000000000, -6.866613759074853001E-15, 1.000000000000000000 ) ) ;
#15252=VERTEX_POINT ( 'NONE', #12638 ) ;
#15273=ORIENTED_EDGE ( 'NONE', *, *, #8633, .T. ) ;
#15337=ORIENTED_EDGE ( 'NONE', *, *, #7475, .T. ) ;
#15349=CARTESIAN_POINT ( 'NONE',  ( 8.000000000000007105, 0.000000000000000000, 0.000000000000000000 ) ) ;
#15350=ORIENTED_EDGE ( 'NONE', *, *, #28492, .F. ) ;
#15359=AXIS2_PLACEMENT_3D ( 'NONE', #21782, #8099, #10098 ) ;
#15390=ORIENTED_EDGE ( 'NONE', *, *, #8629, .T. ) ;
#15405=VERTEX_POINT ( 'NONE', #1842 ) ;
#15406=CYLINDRICAL_SURFACE ( 'NONE', #35218, 4.800000000000000711 ) ;
#15409=ORIENTED_EDGE ( 'NONE', *, *, #11636, .T. ) ;
#15420=ADVANCED_FACE ( 'NONE', ( #10644 ), #2558, .T. ) ;
#15437=AXIS2_PLACEMENT_3D ( 'NONE', #16648, #26235, #1937 ) ;
#15494=VECTOR ( 'NONE', #5223, 1000.000000000000000 ) ;
#15511=DIRECTION ( 'NONE',  ( -1.000000000000000000, 0.000000000000000000, 0.000000000000000000 ) ) ;
#15520=CIRCLE ( 'NONE', #6336, 9.499000000000009436 ) ;
#15523=VERTEX_POINT ( 'NONE', #10828 ) ;
#15542=CIRCLE ( 'NONE', #34544, 9.499000000000000554 ) ;
#15562=ORIENTED_EDGE ( 'NONE', *, *, #19417, .T. ) ;
#15569=CIRCLE ( 'NONE', #4719, 13.99999999999999645 ) ;
#15572=EDGE_LOOP ( 'NONE', ( #32119, #10020, #17080, #29330 ) ) ;
#15606=DIRECTION ( 'NONE',  ( 0.000000000000000000, 0.8660254037844362651, 0.5000000000000041078 ) ) ;
#15612=EDGE_CURVE ( 'NONE', #25092, #20425, #2908, .T. ) ;
#15645=ORIENTED_EDGE ( 'NONE', *, *, #32661, .T. ) ;
#15678=EDGE_CURVE ( 'NONE', #33648, #10684, #21720, .T. ) ;
#15695=EDGE_CURVE ( 'NONE', #23680, #15252, #23931, .T. ) ;
#15703=VERTEX_POINT ( 'NONE', #12765 ) ;
#15712=( NAMED_UNIT ( * ) PLANE_ANGLE_UNIT ( ) SI_UNIT ( $, .RADIAN. ) );
#15732=DIRECTION ( 'NONE',  ( -1.000000000000000000, 0.000000000000000000, 0.000000000000000000 ) ) ;
#15746=AXIS2_PLACEMENT_3D ( 'NONE', #20863, #31865, #7196 ) ;
#15758=LINE ( 'NONE', #21348, #10482 ) ;
#15782=EDGE_LOOP ( 'NONE', ( #9472, #12444, #11154, #35488 ) ) ;
#15792=DIRECTION ( 'NONE',  ( -1.000000000000000000, 0.000000000000000000, 0.000000000000000000 ) ) ;
#15820=EDGE_CURVE ( 'NONE', #26535, #23109, #25187, .T. ) ;
#15830=EDGE_CURVE ( 'NONE', #24024, #22936, #30044, .T. ) ;
#15846=CIRCLE ( 'NONE', #31384, 13.99999999999999645 ) ;
#15867=EDGE_CURVE ( 'NONE', #20005, #27414, #16150, .T. ) ;
#15881=ORIENTED_EDGE ( 'NONE', *, *, #18882, .F. ) ;
#15882=CIRCLE ( 'NONE', #7256, 4.799999999999998934 ) ;
#15913=ORIENTED_EDGE ( 'NONE', *, *, #19414, .T. ) ;
#15918=CARTESIAN_POINT ( 'NONE',  ( -9.999999999999994671, 0.000000000000000000, 0.000000000000000000 ) ) ;
#15942=VECTOR ( 'NONE', #16720, 1000.000000000000000 ) ;
#15957=DIRECTION ( 'NONE',  ( 1.000000000000000000, -0.000000000000000000, -0.000000000000000000 ) ) ;
#15967=AXIS2_PLACEMENT_3D ( 'NONE', #34551, #17960, #9516 ) ;
#15972=CARTESIAN_POINT ( 'NONE',  ( 8.000000000000007105, 11.27190672109280811, -0.3151488735047974776 ) ) ;
#15985=DIRECTION ( 'NONE',  ( 0.000000000000000000, 0.000000000000000000, 1.000000000000000000 ) ) ;
#16008=VERTEX_POINT ( 'NONE', #17389 ) ;
#16023=ORIENTED_EDGE ( 'NONE', *, *, #12416, .F. ) ;
#16055=CARTESIAN_POINT ( 'NONE',  ( 7.999999999999992895, 4.898587196589412829E-16, -4.000000000000000000 ) ) ;
#16079=DIRECTION ( 'NONE',  ( 0.000000000000000000, 0.000000000000000000, 1.000000000000000000 ) ) ;
#16084=DIRECTION ( 'NONE',  ( 0.000000000000000000, -0.5000000000000068834, 0.8660254037844347108 ) ) ;
#16093=DIRECTION ( 'NONE',  ( -1.000000000000000000, 0.000000000000000000, 0.000000000000000000 ) ) ;
#16094=CARTESIAN_POINT ( 'NONE',  ( 8.000000000000007105, -10.15474465512038194, -9.637487275701211331 ) ) ;
#16097=ORIENTED_EDGE ( 'NONE', *, *, #26960, .T. ) ;
#16114=EDGE_CURVE ( 'NONE', #27258, #375, #10017, .T. ) ;
#16132=ORIENTED_EDGE ( 'NONE', *, *, #13227, .T. ) ;
#16138=DIRECTION ( 'NONE',  ( 0.000000000000000000, 0.000000000000000000, 1.000000000000000000 ) ) ;
#16139=CYLINDRICAL_SURFACE ( 'NONE', #25732, 4.000000000000000000 ) ;
#16150=LINE ( 'NONE', #16326, #10227 ) ;
#16159=AXIS2_PLACEMENT_3D ( 'NONE', #6323, #11385, #23054 ) ;
#16160=MECHANICAL_DESIGN_GEOMETRIC_PRESENTATION_REPRESENTATION('',(#11578),#30002);
#16168=DIRECTION ( 'NONE',  ( -1.000000000000000000, 0.000000000000000000, 0.000000000000000000 ) ) ;
#16175=CARTESIAN_POINT ( 'NONE',  ( 0.000000000000000000, -11.27190672109260028, 4.484851126495120077 ) ) ;
#16196=VERTEX_POINT ( 'NONE', #29112 ) ;
#16200=CARTESIAN_POINT ( 'NONE',  ( 8.000000000000007105, 13.42368113696688958, -3.975523202427861058 ) ) ;
#16201=ORIENTED_EDGE ( 'NONE', *, *, #1344, .F. ) ;
#16207=AXIS2_PLACEMENT_3D ( 'NONE', #802, #12323, #8902 ) ;
#16211=FACE_OUTER_BOUND ( 'NONE', #16377, .T. ) ;
#16232=VERTEX_POINT ( 'NONE', #10692 ) ;
#16272=VECTOR ( 'NONE', #25712, 1000.000000000000000 ) ;
#16290=ORIENTED_EDGE ( 'NONE', *, *, #5046, .F. ) ;
#16307=AXIS2_PLACEMENT_3D ( 'NONE', #34233, #29005, #26497 ) ;
#16312=EDGE_CURVE ( 'NONE', #21466, #22617, #35583, .T. ) ;
#16316=CYLINDRICAL_SURFACE ( 'NONE', #32007, 9.499000000000000554 ) ;
#16317=DIRECTION ( 'NONE',  ( -1.000000000000000000, 0.000000000000000000, 0.000000000000000000 ) ) ;
#16319=EDGE_LOOP ( 'NONE', ( #1572, #7222, #4624, #755 ) ) ;
#16326=CARTESIAN_POINT ( 'NONE',  ( 4.000000000000003553, -13.61301047812905907, -3.268936481846298925 ) ) ;
#16332=CIRCLE ( 'NONE', #31875, 4.800000000000000711 ) ;
#16352=CARTESIAN_POINT ( 'NONE',  ( 8.000000000000007105, 0.000000000000000000, 0.000000000000000000 ) ) ;
#16377=EDGE_LOOP ( 'NONE', ( #5025, #9694, #27580, #9710 ) ) ;
#16427=ADVANCED_FACE ( 'NONE', ( #14261 ), #25440, .T. ) ;
#16436=AXIS2_PLACEMENT_3D ( 'NONE', #7961, #5632, #32987 ) ;
#16470=AXIS2_PLACEMENT_3D ( 'NONE', #254, #2448, #2815 ) ;
#16471=CARTESIAN_POINT ( 'NONE',  ( 8.000000000000007105, 0.000000000000000000, 0.000000000000000000 ) ) ;
#16479=AXIS2_PLACEMENT_3D ( 'NONE', #27281, #2623, #252 ) ;
#16483=DIRECTION ( 'NONE',  ( -1.000000000000000000, 0.000000000000000000, 0.000000000000000000 ) ) ;
#16495=ORIENTED_EDGE ( 'NONE', *, *, #3094, .F. ) ;
#16497=AXIS2_PLACEMENT_3D ( 'NONE', #25714, #1221, #33991 ) ;
#16500=CIRCLE ( 'NONE', #34937, 4.800000000000000711 ) ;
#16501=CARTESIAN_POINT ( 'NONE',  ( 50.00005079999998969, 0.000000000000000000, 0.000000000000000000 ) ) ;
#16502=ORIENTED_EDGE ( 'NONE', *, *, #6251, .T. ) ;
#16511=VECTOR ( 'NONE', #17477, 1000.000000000000000 ) ;
#16519=ORIENTED_EDGE ( 'NONE', *, *, #31720, .T. ) ;
#16526=VERTEX_POINT ( 'NONE', #12099 ) ;
#16550=ORIENTED_EDGE ( 'NONE', *, *, #14980, .F. ) ;
#16558=EDGE_CURVE ( 'NONE', #10643, #31978, #11606, .T. ) ;
#16585=DIRECTION ( 'NONE',  ( -1.000000000000000000, 0.000000000000000000, 0.000000000000000000 ) ) ;
#16589=DIRECTION ( 'NONE',  ( 0.000000000000000000, 1.000000000000000000, 3.497202527569241525E-15 ) ) ;
#16606=PRESENTATION_STYLE_ASSIGNMENT (( #19813 ) ) ;
#16648=CARTESIAN_POINT ( 'NONE',  ( 8.000000000000007105, 0.000000000000000000, 0.000000000000000000 ) ) ;
#16658=CARTESIAN_POINT ( 'NONE',  ( 50.00005079999998969, 0.000000000000000000, 4.000000000000000000 ) ) ;
#16676=ORIENTED_EDGE ( 'NONE', *, *, #13962, .T. ) ;
#16682=EDGE_LOOP ( 'NONE', ( #16502, #29598, #7524, #8746 ) ) ;
#16690=ORIENTED_EDGE ( 'NONE', *, *, #1316, .F. ) ;
#16720=DIRECTION ( 'NONE',  ( 1.000000000000000000, -0.000000000000000000, -0.000000000000000000 ) ) ;
#16726=CARTESIAN_POINT ( 'NONE',  ( 8.000000000000007105, 9.604183132802424083, -5.908880290975567995 ) ) ;
#16750=LINE ( 'NONE', #32803, #30206 ) ;
#16756=DIRECTION ( 'NONE',  ( 0.000000000000000000, 0.000000000000000000, -1.000000000000000000 ) ) ;
#16765=ADVANCED_FACE ( 'NONE', ( #19305 ), #22017, .T. ) ;
#16769=CARTESIAN_POINT ( 'NONE',  ( 8.000000000000007105, -5.363026430117032284, -9.919332006307277183 ) ) ;
#16774=SURFACE_SIDE_STYLE ('',( #28133 ) ) ;
#16783=AXIS2_PLACEMENT_3D ( 'NONE', #16471, #2646, #21887 ) ;
#16801=DIRECTION ( 'NONE',  ( 0.000000000000000000, 0.000000000000000000, 1.000000000000000000 ) ) ;
#16827=CARTESIAN_POINT ( 'NONE',  ( 0.000000000000000000, 0.000000000000000000, 0.000000000000000000 ) ) ;
#16868=DIRECTION ( 'NONE',  ( -1.000000000000000000, 0.000000000000000000, 0.000000000000000000 ) ) ;
#16876=FACE_OUTER_BOUND ( 'NONE', #24453, .T. ) ;
#16898=VECTOR ( 'NONE', #13332, 1000.000000000000000 ) ;
#16907=EDGE_LOOP ( 'NONE', ( #15337, #16097, #8719, #20793 ) ) ;
#16923=VERTEX_POINT ( 'NONE', #18610 ) ;
#16937=VERTEX_POINT ( 'NONE', #409 ) ;
#16938=DIRECTION ( 'NONE',  ( -1.000000000000000000, 0.000000000000000000, 0.000000000000000000 ) ) ;
#16961=ADVANCED_FACE ( 'NONE', ( #14263 ), #24908, .T. ) ;
#16969=CARTESIAN_POINT ( 'NONE',  ( 0.000000000000000000, 13.61301047812919762, -3.268936481846202113 ) ) ;
#16973=FACE_OUTER_BOUND ( 'NONE', #12878, .T. ) ;
#16975=AXIS2_PLACEMENT_3D ( 'NONE', #34856, #29274, #32317 ) ;
#16985=CARTESIAN_POINT ( 'NONE',  ( 0.000000000000000000, 9.433698091065187086, -1.111908866155128628 ) ) ;
#17023=CARTESIAN_POINT ( 'NONE',  ( 0.000000000000000000, -13.61301047812919762, 3.268936481846118625 ) ) ;
#17028=DIRECTION ( 'NONE',  ( 0.000000000000000000, 0.000000000000000000, -1.000000000000000000 ) ) ;
#17064=ORIENTED_EDGE ( 'NONE', *, *, #30673, .T. ) ;
#17080=ORIENTED_EDGE ( 'NONE', *, *, #9664, .T. ) ;
#17100=AXIS2_PLACEMENT_3D ( 'NONE', #25275, #11583, #22913 ) ;
#17111=AXIS2_PLACEMENT_3D ( 'NONE', #18868, #15792, #10248 ) ;
#17118=AXIS2_PLACEMENT_3D ( 'NONE', #530, #28084, #3427 ) ;
#17134=EDGE_CURVE ( 'NONE', #23024, #10424, #29297, .T. ) ;
#17140=CARTESIAN_POINT ( 'NONE',  ( 8.000000000000007105, -3.975523202427916125, -13.42368113696675636 ) ) ;
#17149=CARTESIAN_POINT ( 'NONE',  ( 0.000000000000000000, 5.400000000000113154, 0.000000000000000000 ) ) ;
#17158=CARTESIAN_POINT ( 'NONE',  ( 50.00005079999998969, 0.000000000000000000, 0.000000000000000000 ) ) ;
#17176=EDGE_CURVE ( 'NONE', #15252, #620, #23526, .T. ) ;
#17190=DIRECTION ( 'NONE',  ( -1.000000000000000000, 0.000000000000000000, 0.000000000000000000 ) ) ;
#17192=CARTESIAN_POINT ( 'NONE',  ( 0.000000000000000000, 5.363026430117337817, -9.919332006307165273 ) ) ;
#17226=DIRECTION ( 'NONE',  ( 0.000000000000000000, 0.000000000000000000, -1.000000000000000000 ) ) ;
#17282=ORIENTED_EDGE ( 'NONE', *, *, #15820, .T. ) ;
#17294=CIRCLE ( 'NONE', #21339, 4.800000000000000711 ) ;
#17305=ORIENTED_EDGE ( 'NONE', *, *, #9673, .F. ) ;
#17308=DIRECTION ( 'NONE',  ( -1.000000000000000000, 0.000000000000000000, 0.000000000000000000 ) ) ;
#17348=FACE_OUTER_BOUND ( 'NONE', #1435, .T. ) ;
#17355=FACE_OUTER_BOUND ( 'NONE', #16319, .T. ) ;
#17374=EDGE_CURVE ( 'NONE', #33223, #6287, #27003, .T. ) ;
#17389=CARTESIAN_POINT ( 'NONE',  ( 0.000000000000000000, 8.725776631572770725, -3.753907720748954180 ) ) ;
#17426=ORIENTED_EDGE ( 'NONE', *, *, #31720, .F. ) ;
#17434=VERTEX_POINT ( 'NONE', #32216 ) ;
#17438=DIRECTION ( 'NONE',  ( -1.000000000000000000, 0.000000000000000000, 0.000000000000000000 ) ) ;
#17458=DIRECTION ( 'NONE',  ( 0.000000000000000000, 0.000000000000000000, 1.000000000000000000 ) ) ;
#17477=DIRECTION ( 'NONE',  ( -1.000000000000000000, 0.000000000000000000, 0.000000000000000000 ) ) ;
#17480=VERTEX_POINT ( 'NONE', #24471 ) ;
#17509=CARTESIAN_POINT ( 'NONE',  ( 8.000000000000007105, -0.3151488735046864553, -11.27190672109269798 ) ) ;
#17516=CARTESIAN_POINT ( 'NONE',  ( 4.000000000000003553, -13.42368113696669418, 3.975523202427999614 ) ) ;
#17534=DIRECTION ( 'NONE',  ( -1.000000000000000000, 0.000000000000000000, 0.000000000000000000 ) ) ;
#17549=CARTESIAN_POINT ( 'NONE',  ( 8.000000000000007105, -11.27190672109260028, -0.3151488735048807444 ) ) ;
#17550=CARTESIAN_POINT ( 'NONE',  ( 8.000000000000007105, 0.000000000000000000, 0.000000000000000000 ) ) ;
#17551=VERTEX_POINT ( 'NONE', #27873 ) ;
#17591=CIRCLE ( 'NONE', #24512, 4.000000000000000000 ) ;
#17596=CYLINDRICAL_SURFACE ( 'NONE', #31903, 4.800000000000000711 ) ;
#17603=CARTESIAN_POINT ( 'NONE',  ( 8.000000000000007105, 0.3151488735050472778, -11.27190672109269087 ) ) ;
#17605=CIRCLE ( 'NONE', #34918, 9.499000000000004107 ) ;
#17627=CIRCLE ( 'NONE', #2149, 4.800000000000006040 ) ;
#17628=CIRCLE ( 'NONE', #2151, 4.800000000000006040 ) ;
#17629=EDGE_CURVE ( 'NONE', #27414, #19486, #22381, .T. ) ;
#17632=CIRCLE ( 'NONE', #11332, 4.800000000000000711 ) ;
#17643=VERTEX_POINT ( 'NONE', #2875 ) ;
#17652=CIRCLE ( 'NONE', #1556, 14.00000000000000000 ) ;
#17661=CIRCLE ( 'NONE', #31474, 14.00000000000000000 ) ;
#17726=CIRCLE ( 'NONE', #29839, 4.000000000000000000 ) ;
#17742=ORIENTED_EDGE ( 'NONE', *, *, #544, .T. ) ;
#17763=DIRECTION ( 'NONE',  ( -1.000000000000000000, 0.000000000000000000, 0.000000000000000000 ) ) ;
#17786=EDGE_CURVE ( 'NONE', #26887, #5109, #13635, .T. ) ;
#17787=VERTEX_POINT ( 'NONE', #1045 ) ;
#17788=CIRCLE ( 'NONE', #2867, 4.800000000000000711 ) ;
#17806=DIRECTION ( 'NONE',  ( 0.000000000000000000, 0.000000000000000000, -1.000000000000000000 ) ) ;
#17849=ORIENTED_EDGE ( 'NONE', *, *, #9962, .T. ) ;
#17857=EDGE_CURVE ( 'NONE', #7400, #22893, #21665, .T. ) ;
#17886=VERTEX_POINT ( 'NONE', #35074 ) ;
#17928=CARTESIAN_POINT ( 'NONE',  ( 8.000000000000007105, -3.753907720748892007, -8.725776631572756514 ) ) ;
#17960=DIRECTION ( 'NONE',  ( -1.000000000000000000, 0.000000000000000000, 0.000000000000000000 ) ) ;
#17987=DIRECTION ( 'NONE',  ( -1.000000000000000000, 0.000000000000000000, 0.000000000000000000 ) ) ;
#17992=SURFACE_STYLE_USAGE ( .BOTH. , #12613 ) ;
#18037=CYLINDRICAL_SURFACE ( 'NONE', #7253, 13.99999999999999822 ) ;
#18039=CIRCLE ( 'NONE', #14558, 9.499000000000000554 ) ;
#18077=ORIENTED_EDGE ( 'NONE', *, *, #24468, .T. ) ;
#18086=AXIS2_PLACEMENT_3D ( 'NONE', #19721, #28043, #17028 ) ;
#18090=EDGE_LOOP ( 'NONE', ( #8808, #27288, #14062, #31756 ) ) ;
#18145=DIRECTION ( 'NONE',  ( 0.000000000000000000, 0.000000000000000000, 1.000000000000000000 ) ) ;
#18167=DIRECTION ( 'NONE',  ( 0.000000000000000000, 0.8660254037844362651, 0.5000000000000042188 ) ) ;
#18174=SURFACE_STYLE_FILL_AREA ( #28457 ) ;
#18183=CARTESIAN_POINT ( 'NONE',  ( 0.000000000000000000, 11.27190672109280811, -0.3151488735047974776 ) ) ;
#18240=CARTESIAN_POINT ( 'NONE',  ( 8.000000000000007105, -9.604183132802312173, -5.908880290975638161 ) ) ;
#18263=CYLINDRICAL_SURFACE ( 'NONE', #11630, 9.499000000000000554 ) ;
#18285=DIRECTION ( 'NONE',  ( 0.000000000000000000, 0.000000000000000000, 1.000000000000000000 ) ) ;
#18292=DIRECTION ( 'NONE',  ( 1.000000000000000000, 0.000000000000000000, 0.000000000000000000 ) ) ;
#18302=ORIENTED_EDGE ( 'NONE', *, *, #6638, .F. ) ;
#18303=DIRECTION ( 'NONE',  ( -1.000000000000000000, 0.000000000000000000, 0.000000000000000000 ) ) ;
#18321=EDGE_CURVE ( 'NONE', #1657, #21466, #18396, .T. ) ;
#18330=ORIENTED_EDGE ( 'NONE', *, *, #26960, .F. ) ;
#18335=ADVANCED_FACE ( 'NONE', ( #17355 ), #6746, .T. ) ;
#18364=ORIENTED_EDGE ( 'NONE', *, *, #13569, .F. ) ;
#18371=VERTEX_POINT ( 'NONE', #27404 ) ;
#18383=VERTEX_POINT ( 'NONE', #13361 ) ;
#18396=LINE ( 'NONE', #29398, #1671 ) ;
#18430=CIRCLE ( 'NONE', #2937, 4.800000000000000711 ) ;
#18448=CYLINDRICAL_SURFACE ( 'NONE', #24016, 4.800000000000000711 ) ;
#18493=CARTESIAN_POINT ( 'NONE',  ( 8.000000000000007105, -9.604183132802424083, 5.908880290975512928 ) ) ;
#18500=DIRECTION ( 'NONE',  ( 0.000000000000000000, 0.000000000000000000, 1.000000000000000000 ) ) ;
#18507=VERTEX_POINT ( 'NONE', #5615 ) ;
#18511=CIRCLE ( 'NONE', #3011, 9.499000000000004107 ) ;
#18536=EDGE_LOOP ( 'NONE', ( #19585, #20266, #1412, #22751 ) ) ;
#18543=CIRCLE ( 'NONE', #22007, 13.99999999999999645 ) ;
#18561=CARTESIAN_POINT ( 'NONE',  ( 8.000000000000007105, -9.604183132802312173, -5.908880290975638161 ) ) ;
#18582=AXIS2_PLACEMENT_3D ( 'NONE', #17509, #33550, #16801 ) ;
#18583=ORIENTED_EDGE ( 'NONE', *, *, #32353, .T. ) ;
#18594=CARTESIAN_POINT ( 'NONE',  ( 8.000000000000007105, -3.753907720748892007, -8.725776631572756514 ) ) ;
#18609=CIRCLE ( 'NONE', #26673, 9.499000000000012989 ) ;
#18610=CARTESIAN_POINT ( 'NONE',  ( 0.000000000000000000, -13.42368113696669418, 3.975523202427999614 ) ) ;
#18616=DIRECTION ( 'NONE',  ( -1.000000000000000000, 0.000000000000000000, 0.000000000000000000 ) ) ;
#18618=CARTESIAN_POINT ( 'NONE',  ( 8.000000000000007105, 0.000000000000000000, 0.000000000000000000 ) ) ;
#18634=ORIENTED_EDGE ( 'NONE', *, *, #26417, .T. ) ;
#18637=CIRCLE ( 'NONE', #19764, 9.499000000000007660 ) ;
#18683=AXIS2_PLACEMENT_3D ( 'NONE', #8736, #11111, #27507 ) ;
#18721=CARTESIAN_POINT ( 'NONE',  ( 8.000000000000007105, 0.000000000000000000, 0.000000000000000000 ) ) ;
#18724=ORIENTED_EDGE ( 'NONE', *, *, #12555, .F. ) ;
#18729=ORIENTED_EDGE ( 'NONE', *, *, #16312, .F. ) ;
#18799=EDGE_CURVE ( 'NONE', #13248, #19516, #30924, .T. ) ;
#18805=DIRECTION ( 'NONE',  ( -1.000000000000000000, 0.000000000000000000, 0.000000000000000000 ) ) ;
#18807=LINE ( 'NONE', #13413, #5918 ) ;
#18812=CARTESIAN_POINT ( 'NONE',  ( 0.000000000000000000, 0.000000000000000000, 0.000000000000000000 ) ) ;
#18817=VECTOR ( 'NONE', #18805, 1000.000000000000000 ) ;
#18825=ORIENTED_EDGE ( 'NONE', *, *, #29068, .F. ) ;
#18831=AXIS2_PLACEMENT_3D ( 'NONE', #6411, #19713, #14328 ) ;
#18834=EDGE_LOOP ( 'NONE', ( #11558, #21949, #26519, #18724 ) ) ;
#18857=DIRECTION ( 'NONE',  ( -1.000000000000000000, 0.000000000000000000, -0.000000000000000000 ) ) ;
#18868=CARTESIAN_POINT ( 'NONE',  ( 0.000000000000000000, 0.000000000000000000, 0.000000000000000000 ) ) ;
#18882=EDGE_CURVE ( 'NONE', #18371, #22842, #9648, .T. ) ;
#18892=ORIENTED_EDGE ( 'NONE', *, *, #30965, .F. ) ;
#18906=DIRECTION ( 'NONE',  ( -1.000000000000000000, 0.000000000000000000, 0.000000000000000000 ) ) ;
#18972=EDGE_CURVE ( 'NONE', #22936, #19114, #17726, .T. ) ;
#18982=CARTESIAN_POINT ( 'NONE',  ( 8.000000000000007105, -5.908880290975456973, -9.604183132802479150 ) ) ;
#18988=FACE_OUTER_BOUND ( 'NONE', #16682, .T. ) ;
#18995=ORIENTED_EDGE ( 'NONE', *, *, #13962, .F. ) ;
#19073=ORIENTED_EDGE ( 'NONE', *, *, #6635, .F. ) ;
#19079=CIRCLE ( 'NONE', #2997, 14.00000000000000000 ) ;
#19101=AXIS2_PLACEMENT_3D ( 'NONE', #29474, #11262, #3002 ) ;
#19106=DIRECTION ( 'NONE',  ( 0.000000000000000000, 0.000000000000000000, 1.000000000000000000 ) ) ;
#19114=VERTEX_POINT ( 'NONE', #15217 ) ;
#19142=CARTESIAN_POINT ( 'NONE',  ( 8.000000000000007105, 0.000000000000000000, 0.000000000000000000 ) ) ;
#19155=CYLINDRICAL_SURFACE ( 'NONE', #1565, 13.99999999999999822 ) ;
#19219=CARTESIAN_POINT ( 'NONE',  ( -9.999999999999994671, 0.000000000000000000, 0.000000000000000000 ) ) ;
#19237=VERTEX_POINT ( 'NONE', #26773 ) ;
#19264=ORIENTED_EDGE ( 'NONE', *, *, #9258, .F. ) ;
#19280=LINE ( 'NONE', #8128, #32087 ) ;
#19305=FACE_OUTER_BOUND ( 'NONE', #10431, .T. ) ;
#19361=LINE ( 'NONE', #16658, #22278 ) ;
#19364=ADVANCED_FACE ( 'NONE', ( #6033 ), #14471, .T. ) ;
#19369=CARTESIAN_POINT ( 'NONE',  ( 0.000000000000000000, 13.42368113696682030, 3.975523202428055125 ) ) ;
#19374=DIRECTION ( 'NONE',  ( 0.000000000000000000, 0.4999999999999951150, 0.8660254037844414832 ) ) ;
#19385=ORIENTED_EDGE ( 'NONE', *, *, #9409, .T. ) ;
#19395=CARTESIAN_POINT ( 'NONE',  ( 8.000000000000007105, 9.604183132802424083, -1.108880290975567950 ) ) ;
#19396=CARTESIAN_POINT ( 'NONE',  ( 50.00005079999998969, 3.872983346207420574, -1.000000000000000888 ) ) ;
#19398=CYLINDRICAL_SURFACE ( 'NONE', #20187, 9.499000000000000554 ) ;
#19403=DIRECTION ( 'NONE',  ( -1.000000000000000000, 0.000000000000000000, 0.000000000000000000 ) ) ;
#19414=EDGE_CURVE ( 'NONE', #15405, #10684, #455, .T. ) ;
#19417=EDGE_CURVE ( 'NONE', #17643, #18383, #30971, .T. ) ;
#19438=AXIS2_PLACEMENT_3D ( 'NONE', #32045, #7188, #18167 ) ;
#19444=ORIENTED_EDGE ( 'NONE', *, *, #13903, .T. ) ;
#19451=ADVANCED_FACE ( 'NONE', ( #27830 ), #8900, .T. ) ;
#19452=DIRECTION ( 'NONE',  ( 0.000000000000000000, 0.000000000000000000, 1.000000000000000000 ) ) ;
#19457=ADVANCED_FACE ( 'NONE', ( #17348 ), #28350, .T. ) ;
#19468=ORIENTED_EDGE ( 'NONE', *, *, #9991, .F. ) ;
#19486=VERTEX_POINT ( 'NONE', #23170 ) ;
#19491=DIRECTION ( 'NONE',  ( 0.000000000000000000, 0.000000000000000000, 1.000000000000000000 ) ) ;
#19503=CARTESIAN_POINT ( 'NONE',  ( 0.000000000000000000, 8.725776631572825792, 3.753907720749072308 ) ) ;
#19516=VERTEX_POINT ( 'NONE', #12735 ) ;
#19521=DIRECTION ( 'NONE',  ( 0.000000000000000000, 0.000000000000000000, 1.000000000000000000 ) ) ;
#19533=DIRECTION ( 'NONE',  ( 0.000000000000000000, -1.000000000000000000, -1.049160758270772931E-14 ) ) ;
#19536=DIRECTION ( 'NONE',  ( 0.000000000000000000, -0.5000000000000068834, 0.8660254037844347108 ) ) ;
#19538=FACE_OUTER_BOUND ( 'NONE', #5321, .T. ) ;
#19541=EDGE_LOOP ( 'NONE', ( #19980, #919, #32728, #2632 ) ) ;
#19577=DIRECTION ( 'NONE',  ( -1.000000000000000000, 0.000000000000000000, 0.000000000000000000 ) ) ;
#19585=ORIENTED_EDGE ( 'NONE', *, *, #22765, .F. ) ;
#19592=DIRECTION ( 'NONE',  ( 1.000000000000000000, -0.000000000000000000, -0.000000000000000000 ) ) ;
#19627=DIRECTION ( 'NONE',  ( 0.000000000000000000, 0.000000000000000000, 1.000000000000000000 ) ) ;
#19630=DIRECTION ( 'NONE',  ( -1.000000000000000000, 0.000000000000000000, 0.000000000000000000 ) ) ;
#19694=CIRCLE ( 'NONE', #28932, 4.800000000000000711 ) ;
#19713=DIRECTION ( 'NONE',  ( -1.000000000000000000, 0.000000000000000000, 0.000000000000000000 ) ) ;
#19714=ORIENTED_EDGE ( 'NONE', *, *, #7577, .F. ) ;
#19721=CARTESIAN_POINT ( 'NONE',  ( 0.000000000000000000, 9.604183132802452505, 5.908880290975567995 ) ) ;
#19731=CARTESIAN_POINT ( 'NONE',  ( 8.000000000000007105, 7.613867765417669631, 5.679790370316101011 ) ) ;
#19736=CARTESIAN_POINT ( 'NONE',  ( 0.000000000000000000, 5.908880290975762506, -9.604183132802354805 ) ) ;
#19740=AXIS2_PLACEMENT_3D ( 'NONE', #32131, #1712, #7461 ) ;
#19746=DIRECTION ( 'NONE',  ( -1.000000000000000000, 0.000000000000000000, 0.000000000000000000 ) ) ;
#19763=CARTESIAN_POINT ( 'NONE',  ( 0.000000000000000000, 0.000000000000000000, 0.000000000000000000 ) ) ;
#19764=AXIS2_PLACEMENT_3D ( 'NONE', #8055, #5021, #15606 ) ;
#19798=ORIENTED_EDGE ( 'NONE', *, *, #28005, .T. ) ;
#19813=SURFACE_STYLE_USAGE ( .BOTH. , #16774 ) ;
#19820=EDGE_LOOP ( 'NONE', ( #18302, #12455, #32062, #30783, #25776, #33050 ) ) ;
#19833=AXIS2_PLACEMENT_3D ( 'NONE', #22866, #727, #1267 ) ;
#19842=LINE ( 'NONE', #3149, #30082 ) ;
#19863=EDGE_CURVE ( 'NONE', #10643, #34202, #14653, .T. ) ;
#19913=VECTOR ( 'NONE', #11147, 1000.000000000000000 ) ;
#19915=CARTESIAN_POINT ( 'NONE',  ( 8.000000000000007105, 8.725776631572825792, 3.753907720749072308 ) ) ;
#19931=CARTESIAN_POINT ( 'NONE',  ( 0.000000000000000000, 0.000000000000000000, 0.000000000000000000 ) ) ;
#19938=ORIENTED_EDGE ( 'NONE', *, *, #1450, .T. ) ;
#19980=ORIENTED_EDGE ( 'NONE', *, *, #31241, .T. ) ;
#20005=VERTEX_POINT ( 'NONE', #23123 ) ;
#20012=ADVANCED_FACE ( 'NONE', ( #23298 ), #9628, .T. ) ;
#20103=CARTESIAN_POINT ( 'NONE',  ( 8.000000000000007105, -11.27190672109260028, -0.3151488735048807444 ) ) ;
#20144=CYLINDRICAL_SURFACE ( 'NONE', #33519, 9.499000000000000554 ) ;
#20151=CARTESIAN_POINT ( 'NONE',  ( 0.000000000000000000, 0.000000000000000000, 0.000000000000000000 ) ) ;
#20166=VECTOR ( 'NONE', #17438, 1000.000000000000000 ) ;
#20187=AXIS2_PLACEMENT_3D ( 'NONE', #32919, #140, #14343 ) ;
#20190=CARTESIAN_POINT ( 'NONE',  ( 8.000000000000007105, -5.908880290975582206, 9.604183132802395662 ) ) ;
#20227=EDGE_CURVE ( 'NONE', #375, #26423, #22425, .T. ) ;
#20230=AXIS2_PLACEMENT_3D ( 'NONE', #23812, #28852, #34618 ) ;
#20234=AXIS2_PLACEMENT_3D ( 'NONE', #9977, #35196, #24203 ) ;
#20251=CIRCLE ( 'NONE', #24326, 14.00000000000000000 ) ;
#20266=ORIENTED_EDGE ( 'NONE', *, *, #33716, .T. ) ;
#20286=AXIS2_PLACEMENT_3D ( 'NONE', #327, #33452, #33108 ) ;
#20314=ORIENTED_EDGE ( 'NONE', *, *, #3778, .T. ) ;
#20321=LINE ( 'NONE', #29180, #12245 ) ;
#20325=CARTESIAN_POINT ( 'NONE',  ( 8.000000000000007105, 5.363026430117337817, -9.919332006307165273 ) ) ;
#20326=VERTEX_POINT ( 'NONE', #3314 ) ;
#20369=CARTESIAN_POINT ( 'NONE',  ( 0.000000000000000000, -9.919332006307138627, -5.363026430117212584 ) ) ;
#20374=DIRECTION ( 'NONE',  ( 0.000000000000000000, 0.000000000000000000, -1.000000000000000000 ) ) ;
#20414=DIRECTION ( 'NONE',  ( -1.000000000000000000, 0.000000000000000000, 0.000000000000000000 ) ) ;
#20418=CARTESIAN_POINT ( 'NONE',  ( 0.000000000000000000, 3.753907720749211308, -8.725776631572673026 ) ) ;
#20421=LINE ( 'NONE', #26038, #23900 ) ;
#20425=VERTEX_POINT ( 'NONE', #17140 ) ;
#20463=CARTESIAN_POINT ( 'NONE',  ( 8.000000000000007105, 3.753907720749211308, -8.725776631572673026 ) ) ;
#20470=DIRECTION ( 'NONE',  ( 0.000000000000000000, 1.000000000000000000, 3.497202527569241525E-15 ) ) ;
#20471=AXIS2_PLACEMENT_3D ( 'NONE', #475, #25150, #19374 ) ;
#20478=AXIS2_PLACEMENT_3D ( 'NONE', #27844, #17190, #25144 ) ;
#20495=AXIS2_PLACEMENT_3D ( 'NONE', #19142, #18616, #21305 ) ;
#20529=CARTESIAN_POINT ( 'NONE',  ( 8.000000000000007105, 5.908880290975540461, 9.604183132802438294 ) ) ;
#20536=DIRECTION ( 'NONE',  ( -1.000000000000000000, 0.000000000000000000, 0.000000000000000000 ) ) ;
#20595=CARTESIAN_POINT ( 'NONE',  ( 8.000000000000007105, 3.975523202428290936, -13.42368113696666754 ) ) ;
#20607=EDGE_LOOP ( 'NONE', ( #14278, #5032, #28437, #15913 ) ) ;
#20626=ORIENTED_EDGE ( 'NONE', *, *, #32387, .T. ) ;
#20643=DIRECTION ( 'NONE',  ( 0.000000000000000000, 0.000000000000000000, 1.000000000000000000 ) ) ;
#20656=VERTEX_POINT ( 'NONE', #509 ) ;
#20716=ORIENTED_EDGE ( 'NONE', *, *, #15695, .T. ) ;
#20758=VECTOR ( 'NONE', #14183, 1000.000000000000000 ) ;
#20784=AXIS2_PLACEMENT_3D ( 'NONE', #32338, #10737, #13100 ) ;
#20793=ORIENTED_EDGE ( 'NONE', *, *, #15830, .F. ) ;
#20800=ORIENTED_EDGE ( 'NONE', *, *, #9342, .T. ) ;
#20836=CARTESIAN_POINT ( 'NONE',  ( 8.000000000000007105, 0.000000000000000000, 0.000000000000000000 ) ) ;
#20863=CARTESIAN_POINT ( 'NONE',  ( 7.999999999999992895, 0.000000000000000000, 0.000000000000000000 ) ) ;
#20886=AXIS2_PLACEMENT_3D ( 'NONE', #23080, #4205, #31192 ) ;
#20887=ADVANCED_FACE ( 'NONE', ( #1396 ), #12373, .T. ) ;
#20906=CARTESIAN_POINT ( 'NONE',  ( 8.000000000000007105, 5.679790370316226245, -7.613867765417517752 ) ) ;
#20907=AXIS2_PLACEMENT_3D ( 'NONE', #28659, #31349, #12266 ) ;
#20914=EDGE_CURVE ( 'NONE', #17551, #11623, #22072, .T. ) ;
#20927=ORIENTED_EDGE ( 'NONE', *, *, #32301, .F. ) ;
#20938=EDGE_CURVE ( 'NONE', #1909, #15703, #31178, .T. ) ;
#20941=CARTESIAN_POINT ( 'NONE',  ( 0.000000000000000000, 0.000000000000000000, 0.000000000000000000 ) ) ;
#20952=CARTESIAN_POINT ( 'NONE',  ( 0.000000000000000000, 9.637487275701129619, 10.15474465512053470 ) ) ;
#20959=AXIS2_PLACEMENT_3D ( 'NONE', #22434, #30558, #8232 ) ;
#20983=ORIENTED_EDGE ( 'NONE', *, *, #25579, .T. ) ;
#21028=VERTEX_POINT ( 'NONE', #5522 ) ;
#21054=CIRCLE ( 'NONE', #976, 14.00000000000000000 ) ;
#21055=DIRECTION ( 'NONE',  ( -1.000000000000000000, 0.000000000000000000, 0.000000000000000000 ) ) ;
#21092=EDGE_LOOP ( 'NONE', ( #21321, #20314, #18077, #17849 ) ) ;
#21093=CARTESIAN_POINT ( 'NONE',  ( 50.00005079999998969, 5.400000000000098943, 1.000000000000000888 ) ) ;
#21134=AXIS2_PLACEMENT_3D ( 'NONE', #2548, #29902, #30433 ) ;
#21145=FACE_OUTER_BOUND ( 'NONE', #31318, .T. ) ;
#21165=ORIENTED_EDGE ( 'NONE', *, *, #5088, .T. ) ;
#21203=ORIENTED_EDGE ( 'NONE', *, *, #3778, .F. ) ;
#21214=CARTESIAN_POINT ( 'NONE',  ( 8.000000000000007105, 7.613867765417669631, 5.679790370316101011 ) ) ;
#21235=ORIENTED_EDGE ( 'NONE', *, *, #19414, .F. ) ;
#21265=ORIENTED_EDGE ( 'NONE', *, *, #17134, .T. ) ;
#21305=DIRECTION ( 'NONE',  ( 0.000000000000000000, 0.5000000000000011102, -0.8660254037844380415 ) ) ;
#21307=AXIS2_PLACEMENT_3D ( 'NONE', #26589, #12725, #18292 ) ;
#21321=ORIENTED_EDGE ( 'NONE', *, *, #478, .T. ) ;
#21336=VERTEX_POINT ( 'NONE', #20595 ) ;
#21339=AXIS2_PLACEMENT_3D ( 'NONE', #6262, #27875, #22456 ) ;
#21348=CARTESIAN_POINT ( 'NONE',  ( 4.000000000000003553, 10.15474465512070168, -9.637487275700989287 ) ) ;
#21359=AXIS2_PLACEMENT_3D ( 'NONE', #11176, #22147, #19452 ) ;
#21362=AXIS2_PLACEMENT_3D ( 'NONE', #24083, #29116, #10389 ) ;
#21373=CARTESIAN_POINT ( 'NONE',  ( 0.000000000000000000, -9.919332006307262972, 5.363026430117087351 ) ) ;
#21375=EDGE_LOOP ( 'NONE', ( #34611, #26263, #12535, #25709, #13863, #30305, #6027, #11509, #8279, #16132, #10338, #27600, #24085, #27602, #11028, #28568, #11313, #14406, #33990, #28044, #25752, #34682, #28402, #22535, #12490, #29722, #29957, #5770, #1784, #28395, #25387, #6725, #22342, #30702, #32957, #6586, #11246, #22753, #23290, #30628, #20626, #28996, #18995, #25559, #4809, #32084, #4217, #28123, #19798, #30088, #27532, #35061, #33500 ) ) ;
#21411=CYLINDRICAL_SURFACE ( 'NONE', #30166, 9.499000000000000554 ) ;
#21412=ORIENTED_EDGE ( 'NONE', *, *, #16558, .T. ) ;
#21466=VERTEX_POINT ( 'NONE', #2803 ) ;
#21503=DIRECTION ( 'NONE',  ( -1.000000000000000000, 0.000000000000000000, 0.000000000000000000 ) ) ;
#21512=EDGE_CURVE ( 'NONE', #16196, #741, #18609, .T. ) ;
#21554=VECTOR ( 'NONE', #3194, 1000.000000000000000 ) ;
#21557=ORIENTED_EDGE ( 'NONE', *, *, #21889, .T. ) ;
#21610=COLOUR_RGB ( '', 0.72549020, 0.75294118, 0.79215686) ;
#21613=AXIS2_PLACEMENT_3D ( 'NONE', #32150, #8010, #32688 ) ;
#21665=CIRCLE ( 'NONE', #9026, 13.99999999999999645 ) ;
#21678=DIRECTION ( 'NONE',  ( 1.000000000000000000, -0.000000000000000000, -0.000000000000000000 ) ) ;
#21720=CIRCLE ( 'NONE', #17111, 9.499000000000011212 ) ;
#21763=ADVANCED_FACE ( 'NONE', ( #2971 ), #13930, .T. ) ;
#21782=CARTESIAN_POINT ( 'NONE',  ( 8.000000000000007105, -9.919332006307262972, 5.363026430117087351 ) ) ;
#21814=ORIENTED_EDGE ( 'NONE', *, *, #27375, .F. ) ;
#21816=VERTEX_POINT ( 'NONE', #34623 ) ;
#21829=ORIENTED_EDGE ( 'NONE', *, *, #7100, .F. ) ;
#21847=CARTESIAN_POINT ( 'NONE',  ( 0.000000000000000000, 3.975523202428290936, -13.42368113696666754 ) ) ;
#21858=ADVANCED_FACE ( 'NONE', ( #7060 ), #18037, .T. ) ;
#21863=CYLINDRICAL_SURFACE ( 'NONE', #16479, 4.800000000000000711 ) ;
#21872=CARTESIAN_POINT ( 'NONE',  ( 8.000000000000007105, -5.363026430117185051, 9.919332006307207905 ) ) ;
#21887=DIRECTION ( 'NONE',  ( 0.000000000000000000, 0.8660254037844398178, -0.4999999999999977796 ) ) ;
#21889=EDGE_CURVE ( 'NONE', #8987, #25674, #14165, .T. ) ;
#21898=DIRECTION ( 'NONE',  ( 0.000000000000000000, -0.4999999999999890643, -0.8660254037844449249 ) ) ;
#21899=DIRECTION ( 'NONE',  ( 0.000000000000000000, 0.000000000000000000, -1.000000000000000000 ) ) ;
#21905=CIRCLE ( 'NONE', #10996, 4.800000000000000711 ) ;
#21906=COLOUR_RGB ( '', 0.72549020, 0.75294118, 0.79215686) ;
#21924=VERTEX_POINT ( 'NONE', #29930 ) ;
#21928=CIRCLE ( 'NONE', #21359, 13.99999999999999645 ) ;
#21930=CIRCLE ( 'NONE', #11025, 4.000000000000000000 ) ;
#21949=ORIENTED_EDGE ( 'NONE', *, *, #29137, .T. ) ;
#21965=ORIENTED_EDGE ( 'NONE', *, *, #631, .T. ) ;
#21983=DIRECTION ( 'NONE',  ( 0.000000000000000000, 0.8660254037844398178, -0.4999999999999977796 ) ) ;
#21984=CARTESIAN_POINT ( 'NONE',  ( 0.000000000000000000, 0.000000000000000000, 0.000000000000000000 ) ) ;
#21997=CYLINDRICAL_SURFACE ( 'NONE', #7319, 4.800000000000000711 ) ;
#22007=AXIS2_PLACEMENT_3D ( 'NONE', #2110, #21503, #18285 ) ;
#22013=EDGE_CURVE ( 'NONE', #26535, #26887, #32094, .T. ) ;
#22017=CYLINDRICAL_SURFACE ( 'NONE', #27558, 4.799999999999998934 ) ;
#22072=LINE ( 'NONE', #10748, #5845 ) ;
#22087=VERTEX_POINT ( 'NONE', #30626 ) ;
#22096=EDGE_CURVE ( 'NONE', #1657, #17643, #2118, .T. ) ;
#22116=PLANE ( 'NONE',  #22126 ) ;
#22120=DIRECTION ( 'NONE',  ( 0.000000000000000000, 1.000000000000000000, 3.497202527569241525E-15 ) ) ;
#22126=AXIS2_PLACEMENT_3D ( 'NONE', #331, #3898, #33114 ) ;
#22147=DIRECTION ( 'NONE',  ( -1.000000000000000000, 0.000000000000000000, 0.000000000000000000 ) ) ;
#22163=LINE ( 'NONE', #25239, #35290 ) ;
#22236=CARTESIAN_POINT ( 'NONE',  ( 7.999999999999992895, 3.872983346207531596, 1.000000000000000888 ) ) ;
#22242=ADVANCED_FACE ( 'NONE', ( #28814 ), #23224, .T. ) ;
#22248=MANIFOLD_SOLID_BREP ( 'Keyway', #8324 ) ;
#22278=VECTOR ( 'NONE', #32349, 1000.000000000000000 ) ;
#22288=EDGE_CURVE ( 'NONE', #17787, #21924, #17627, .T. ) ;
#22342=ORIENTED_EDGE ( 'NONE', *, *, #32265, .F. ) ;
#22362=ORIENTED_EDGE ( 'NONE', *, *, #10722, .T. ) ;
#22381=CIRCLE ( 'NONE', #4608, 4.800000000000006928 ) ;
#22397=ORIENTED_EDGE ( 'NONE', *, *, #22096, .F. ) ;
#22425=CIRCLE ( 'NONE', #4064, 4.800000000000000711 ) ;
#22430=EDGE_LOOP ( 'NONE', ( #792, #30828, #12595, #33305 ) ) ;
#22434=CARTESIAN_POINT ( 'NONE',  ( 8.000000000000007105, -0.3151488735046864553, -11.27190672109269798 ) ) ;
#22440=EDGE_CURVE ( 'NONE', #1552, #31085, #9305, .T. ) ;
#22444=DIRECTION ( 'NONE',  ( 0.000000000000000000, 0.8660254037844398178, -0.4999999999999978906 ) ) ;
#22456=DIRECTION ( 'NONE',  ( 0.000000000000000000, 0.000000000000000000, -1.000000000000000000 ) ) ;
#22465=CARTESIAN_POINT ( 'NONE',  ( 4.000000000000003553, -9.637487275700962641, -10.15474465512058977 ) ) ;
#22486=ORIENTED_EDGE ( 'NONE', *, *, #1087, .F. ) ;
#22490=VECTOR ( 'NONE', #12806, 1000.000000000000000 ) ;
#22513=CARTESIAN_POINT ( 'NONE',  ( 8.000000000000007105, 9.604183132802424083, -5.908880290975567995 ) ) ;
#22535=ORIENTED_EDGE ( 'NONE', *, *, #29962, .T. ) ;
#22589=DIRECTION ( 'NONE',  ( -1.000000000000000000, 0.000000000000000000, 0.000000000000000000 ) ) ;
#22592=AXIS2_PLACEMENT_3D ( 'NONE', #9133, #14346, #33439 ) ;
#22611=ORIENTED_EDGE ( 'NONE', *, *, #15612, .T. ) ;
#22617=VERTEX_POINT ( 'NONE', #20952 ) ;
#22629=FACE_OUTER_BOUND ( 'NONE', #32462, .T. ) ;
#22633=ADVANCED_FACE ( 'NONE', ( #31953 ), #18263, .T. ) ;
#22647=CARTESIAN_POINT ( 'NONE',  ( 0.000000000000000000, -9.637487275701184686, 10.15474465512046542 ) ) ;
#22685=CARTESIAN_POINT ( 'NONE',  ( 0.000000000000000000, -5.679790370316031733, 7.613867765417587030 ) ) ;
#22688=ORIENTED_EDGE ( 'NONE', *, *, #5011, .T. ) ;
#22695=ADVANCED_FACE ( 'NONE', ( #24218 ), #35209, .T. ) ;
#22735=EDGE_LOOP ( 'NONE', ( #26269, #14322, #21235, #20800 ) ) ;
#22751=ORIENTED_EDGE ( 'NONE', *, *, #26594, .F. ) ;
#22753=ORIENTED_EDGE ( 'NONE', *, *, #2860, .F. ) ;
#22765=EDGE_CURVE ( 'NONE', #24903, #27346, #27975, .T. ) ;
#22792=ORIENTED_EDGE ( 'NONE', *, *, #27375, .T. ) ;
#22796=AXIS2_PLACEMENT_3D ( 'NONE', #17158, #27650, #28167 ) ;
#22820=AXIS2_PLACEMENT_3D ( 'NONE', #18812, #10900, #24401 ) ;
#22832=DIRECTION ( 'NONE',  ( 0.000000000000000000, 0.000000000000000000, 1.000000000000000000 ) ) ;
#22842=VERTEX_POINT ( 'NONE', #16969 ) ;
#22865=ORIENTED_EDGE ( 'NONE', *, *, #21889, .F. ) ;
#22866=CARTESIAN_POINT ( 'NONE',  ( 8.000000000000007105, 5.908880290975762506, -9.604183132802354805 ) ) ;
#22875=EDGE_CURVE ( 'NONE', #15170, #13248, #14816, .T. ) ;
#22893=VERTEX_POINT ( 'NONE', #33907 ) ;
#22898=ORIENTED_EDGE ( 'NONE', *, *, #13450, .T. ) ;
#22901=SHAPE_REPRESENTATION ( 'spur gear_iso_ISO - Spur gear 2M 12T 20PA 8FW ---S12A75H50L8.0S1', ( #21307 ), #27126 ) ;
#22913=DIRECTION ( 'NONE',  ( 0.000000000000000000, -0.8660254037844326014, -0.5000000000000102141 ) ) ;
#22920=CARTESIAN_POINT ( 'NONE',  ( 8.000000000000007105, 0.000000000000000000, 0.000000000000000000 ) ) ;
#22936=VERTEX_POINT ( 'NONE', #4577 ) ;
#22946=EDGE_CURVE ( 'NONE', #33265, #32057, #20251, .T. ) ;
#22984=ORIENTED_EDGE ( 'NONE', *, *, #9856, .T. ) ;
#22986=CARTESIAN_POINT ( 'NONE',  ( 8.000000000000007105, -9.604183132802312173, -1.108880290975637228 ) ) ;
#22990=DIRECTION ( 'NONE',  ( 1.000000000000000000, -0.000000000000000000, 0.000000000000000000 ) ) ;
#23010=DIRECTION ( 'NONE',  ( -1.000000000000000000, 0.000000000000000000, 0.000000000000000000 ) ) ;
#23016=CYLINDRICAL_SURFACE ( 'NONE', #15177, 9.499000000000000554 ) ;
#23024=VERTEX_POINT ( 'NONE', #12664 ) ;
#23050=ORIENTED_EDGE ( 'NONE', *, *, #8077, .F. ) ;
#23054=DIRECTION ( 'NONE',  ( 0.000000000000000000, 0.000000000000000000, 1.000000000000000000 ) ) ;
#23071=ORIENTED_EDGE ( 'NONE', *, *, #29968, .F. ) ;
#23080=CARTESIAN_POINT ( 'NONE',  ( 0.000000000000000000, 0.000000000000000000, 0.000000000000000000 ) ) ;
#23109=VERTEX_POINT ( 'NONE', #2047 ) ;
#23117=EDGE_CURVE ( 'NONE', #17886, #10094, #2404, .T. ) ;
#23123=CARTESIAN_POINT ( 'NONE',  ( 0.000000000000000000, -13.61301047812905907, -3.268936481846298925 ) ) ;
#23138=DIRECTION ( 'NONE',  ( -1.000000000000000000, 0.000000000000000000, 0.000000000000000000 ) ) ;
#23170=CARTESIAN_POINT ( 'NONE',  ( 8.000000000000007105, -9.604183132802312173, -1.108880290975637228 ) ) ;
#23179=DIRECTION ( 'NONE',  ( -1.000000000000000000, 0.000000000000000000, 0.000000000000000000 ) ) ;
#23198=DIRECTION ( 'NONE',  ( -1.000000000000000000, 0.000000000000000000, 0.000000000000000000 ) ) ;
#23224=CYLINDRICAL_SURFACE ( 'NONE', #26228, 13.99999999999999822 ) ;
#23239=CYLINDRICAL_SURFACE ( 'NONE', #646, 4.800000000000000711 ) ;
#23246=ORIENTED_EDGE ( 'NONE', *, *, #9991, .T. ) ;
#23255=VERTEX_POINT ( 'NONE', #26104 ) ;
#23256=CARTESIAN_POINT ( 'NONE',  ( 8.000000000000007105, 0.000000000000000000, 0.000000000000000000 ) ) ;
#23290=ORIENTED_EDGE ( 'NONE', *, *, #17786, .F. ) ;
#23298=FACE_OUTER_BOUND ( 'NONE', #246, .T. ) ;
#23302=EDGE_CURVE ( 'NONE', #19237, #15405, #25477, .T. ) ;
#23307=ORIENTED_EDGE ( 'NONE', *, *, #29426, .T. ) ;
#23359=CARTESIAN_POINT ( 'NONE',  ( 4.000000000000003553, 3.975523202428013381, 13.42368113696675103 ) ) ;
#23402=CIRCLE ( 'NONE', #27457, 14.00000000000000000 ) ;
#23404=ADVANCED_FACE ( 'NONE', ( #2345 ), #24466, .T. ) ;
#23419=CIRCLE ( 'NONE', #29753, 9.499000000000007660 ) ;
#23526=CIRCLE ( 'NONE', #10328, 9.499000000000000554 ) ;
#23602=CARTESIAN_POINT ( 'NONE',  ( 0.000000000000000000, -13.42368113696662490, -3.975523202428152381 ) ) ;
#23630=ADVANCED_FACE ( 'NONE', ( #14698 ), #14513, .T. ) ;
#23659=ORIENTED_EDGE ( 'NONE', *, *, #34721, .F. ) ;
#23660=EDGE_CURVE ( 'NONE', #19486, #26231, #14178, .T. ) ;
#23667=AXIS2_PLACEMENT_3D ( 'NONE', #30565, #33097, #22444 ) ;
#23680=VERTEX_POINT ( 'NONE', #19731 ) ;
#23701=ORIENTED_EDGE ( 'NONE', *, *, #15612, .F. ) ;
#23705=FACE_OUTER_BOUND ( 'NONE', #10532, .T. ) ;
#23732=CARTESIAN_POINT ( 'NONE',  ( 50.00005079999998969, 5.400000000000029665, -1.000000000000000888 ) ) ;
#23798=AXIS2_PLACEMENT_3D ( 'NONE', #18240, #4764, #29245 ) ;
#23812=CARTESIAN_POINT ( 'NONE',  ( 8.000000000000007105, -9.604183132802312173, -5.908880290975638161 ) ) ;
#23820=ADVANCED_FACE ( 'NONE', ( #22629 ), #30933, .T. ) ;
#23835=EDGE_LOOP ( 'NONE', ( #31783, #31302, #30153, #33701 ) ) ;
#23846=CIRCLE ( 'NONE', #3165, 4.800000000000001599 ) ;
#23847=DIRECTION ( 'NONE',  ( -1.000000000000000000, 0.000000000000000000, 0.000000000000000000 ) ) ;
#23850=ADVANCED_FACE ( 'NONE', ( #25900 ), #3943, .T. ) ;
#23888=EDGE_LOOP ( 'NONE', ( #14950, #3807, #20716, #21165 ) ) ;
#23891=CYLINDRICAL_SURFACE ( 'NONE', #20784, 4.800000000000000711 ) ;
#23900=VECTOR ( 'NONE', #1371, 1000.000000000000000 ) ;
#23917=DIRECTION ( 'NONE',  ( 0.000000000000000000, 0.000000000000000000, 1.000000000000000000 ) ) ;
#23931=LINE ( 'NONE', #21214, #7929 ) ;
#23967=ORIENTED_EDGE ( 'NONE', *, *, #12611, .T. ) ;
#23986=CIRCLE ( 'NONE', #32023, 4.800000000000006040 ) ;
#24016=AXIS2_PLACEMENT_3D ( 'NONE', #4790, #15732, #26750 ) ;
#24024=VERTEX_POINT ( 'NONE', #9846 ) ;
#24069=DIRECTION ( 'NONE',  ( 0.000000000000000000, 0.000000000000000000, 1.000000000000000000 ) ) ;
#24083=CARTESIAN_POINT ( 'NONE',  ( 8.000000000000007105, 0.000000000000000000, 0.000000000000000000 ) ) ;
#24085=ORIENTED_EDGE ( 'NONE', *, *, #25939, .F. ) ;
#24108=VERTEX_POINT ( 'NONE', #4998 ) ;
#24185=CIRCLE ( 'NONE', #8642, 9.499000000000009436 ) ;
#24203=DIRECTION ( 'NONE',  ( 0.000000000000000000, 0.000000000000000000, -1.000000000000000000 ) ) ;
#24205=DIRECTION ( 'NONE',  ( 0.000000000000000000, -1.000000000000000000, -1.048062100069320848E-14 ) ) ;
#24218=FACE_OUTER_BOUND ( 'NONE', #12863, .T. ) ;
#24230=FACE_BOUND ( 'NONE', #19820, .T. ) ;
#24324=VERTEX_POINT ( 'NONE', #34085 ) ;
#24326=AXIS2_PLACEMENT_3D ( 'NONE', #7067, #15155, #12296 ) ;
#24358=CIRCLE ( 'NONE', #9385, 9.499000000000004107 ) ;
#24388=CIRCLE ( 'NONE', #8845, 13.99999999999999645 ) ;
#24390=ORIENTED_EDGE ( 'NONE', *, *, #11699, .F. ) ;
#24401=DIRECTION ( 'NONE',  ( 0.000000000000000000, 0.4999999999999948375, 0.8660254037844415942 ) ) ;
#24412=ORIENTED_EDGE ( 'NONE', *, *, #4914, .F. ) ;
#24423=DIRECTION ( 'NONE',  ( -1.000000000000000000, 0.000000000000000000, 0.000000000000000000 ) ) ;
#24434=DIRECTION ( 'NONE',  ( -1.000000000000000000, 0.000000000000000000, 0.000000000000000000 ) ) ;
#24446=DIRECTION ( 'NONE',  ( 0.000000000000000000, 0.000000000000000000, 1.000000000000000000 ) ) ;
#24453=EDGE_LOOP ( 'NONE', ( #30105, #1117, #17742, #18330 ) ) ;
#24466=CYLINDRICAL_SURFACE ( 'NONE', #29520, 13.99999999999999822 ) ;
#24468=EDGE_CURVE ( 'NONE', #18507, #20326, #31906, .T. ) ;
#24471=CARTESIAN_POINT ( 'NONE',  ( 8.000000000000007105, 3.975523202428013381, 13.42368113696675103 ) ) ;
#24512=AXIS2_PLACEMENT_3D ( 'NONE', #29236, #32281, #4580 ) ;
#24541=DIRECTION ( 'NONE',  ( -1.000000000000000000, 0.000000000000000000, 0.000000000000000000 ) ) ;
#24576=CARTESIAN_POINT ( 'NONE',  ( 8.000000000000007105, -11.27190672109268377, 0.3151488735047419665 ) ) ;
#24619=ADVANCED_FACE ( 'NONE', ( #27759 ), #2762, .F. ) ;
#24639=ADVANCED_FACE ( 'NONE', ( #16211 ), #11018, .T. ) ;
#24655=CARTESIAN_POINT ( 'NONE',  ( 8.000000000000007105, 0.000000000000000000, 0.000000000000000000 ) ) ;
#24670=EDGE_CURVE ( 'NONE', #19516, #31085, #14068, .T. ) ;
#24674=EDGE_CURVE ( 'NONE', #31085, #8987, #16750, .T. ) ;
#24682=EDGE_CURVE ( 'NONE', #17551, #27414, #33626, .T. ) ;
#24709=DIRECTION ( 'NONE',  ( 1.000000000000000000, -0.000000000000000000, 0.000000000000000000 ) ) ;
#24743=EDGE_CURVE ( 'NONE', #14025, #15523, #4925, .T. ) ;
#24789=AXIS2_PLACEMENT_3D ( 'NONE', #27499, #29843, #10568 ) ;
#24812=DIRECTION ( 'NONE',  ( -1.000000000000000000, 0.000000000000000000, 0.000000000000000000 ) ) ;
#24872=CIRCLE ( 'NONE', #33493, 4.800000000000005151 ) ;
#24877=DIRECTION ( 'NONE',  ( -1.000000000000000000, 0.000000000000000000, 0.000000000000000000 ) ) ;
#24884=VERTEX_POINT ( 'NONE', #28284 ) ;
#24894=VECTOR ( 'NONE', #31202, 1000.000000000000000 ) ;
#24898=ORIENTED_EDGE ( 'NONE', *, *, #28248, .F. ) ;
#24903=VERTEX_POINT ( 'NONE', #27016 ) ;
#24907=PRODUCT_DEFINITION_CONTEXT ( 'detailed design', #7123, 'design' ) ;
#24908=CYLINDRICAL_SURFACE ( 'NONE', #31005, 4.800000000000000711 ) ;
#24950=DIRECTION ( 'NONE',  ( -1.000000000000000000, 0.000000000000000000, 0.000000000000000000 ) ) ;
#24998=VECTOR ( 'NONE', #690, 1000.000000000000000 ) ;
#25008=FACE_OUTER_BOUND ( 'NONE', #16907, .T. ) ;
#25049=DIRECTION ( 'NONE',  ( -1.000000000000000000, 0.000000000000000000, 0.000000000000000000 ) ) ;
#25077=DIRECTION ( 'NONE',  ( -1.000000000000000000, 0.000000000000000000, 0.000000000000000000 ) ) ;
#25083=AXIS2_PLACEMENT_3D ( 'NONE', #18493, #34363, #15241 ) ;
#25092=VERTEX_POINT ( 'NONE', #5916 ) ;
#25094=CARTESIAN_POINT ( 'NONE',  ( 8.000000000000007105, -3.753907720749058541, 8.725776631572749409 ) ) ;
#25102=CARTESIAN_POINT ( 'NONE',  ( 0.000000000000000000, -9.604183132802312173, -5.908880290975638161 ) ) ;
#25133=DIRECTION ( 'NONE',  ( -0.000000000000000000, 1.000000000000000000, 0.000000000000000000 ) ) ;
#25134=AXIS2_PLACEMENT_3D ( 'NONE', #26984, #29670, #23917 ) ;
#25142=CARTESIAN_POINT ( 'NONE',  ( 8.000000000000007105, 0.000000000000000000, 0.000000000000000000 ) ) ;
#25144=DIRECTION ( 'NONE',  ( 0.000000000000000000, 0.000000000000000000, 1.000000000000000000 ) ) ;
#25150=DIRECTION ( 'NONE',  ( -1.000000000000000000, 0.000000000000000000, 0.000000000000000000 ) ) ;
#25155=CARTESIAN_POINT ( 'NONE',  ( 8.000000000000007105, 3.753907720749211308, -8.725776631572673026 ) ) ;
#25182=DIRECTION ( 'NONE',  ( 0.000000000000000000, -6.866613759074851423E-15, 1.000000000000000000 ) ) ;
#25187=CIRCLE ( 'NONE', #12537, 9.499000000000012989 ) ;
#25211=AXIS2_PLACEMENT_3D ( 'NONE', #229, #17308, #11213 ) ;
#25215=EDGE_LOOP ( 'NONE', ( #9569, #15562, #31491, #32689 ) ) ;
#25239=CARTESIAN_POINT ( 'NONE',  ( 7.999999999999992895, 5.400000000000113154, 0.000000000000000000 ) ) ;
#25246=ORIENTED_EDGE ( 'NONE', *, *, #15867, .T. ) ;
#25259=VERTEX_POINT ( 'NONE', #20463 ) ;
#25275=CARTESIAN_POINT ( 'NONE',  ( 8.000000000000007105, 0.000000000000000000, 0.000000000000000000 ) ) ;
#25300=CARTESIAN_POINT ( 'NONE',  ( 8.000000000000007105, 0.000000000000000000, 0.000000000000000000 ) ) ;
#25309=DIRECTION ( 'NONE',  ( -1.000000000000000000, 0.000000000000000000, 0.000000000000000000 ) ) ;
#25359=DIRECTION ( 'NONE',  ( 0.000000000000000000, 0.000000000000000000, 1.000000000000000000 ) ) ;
#25378=CARTESIAN_POINT ( 'NONE',  ( 8.000000000000007105, -7.613867765417476008, -5.679790370316101011 ) ) ;
#25387=ORIENTED_EDGE ( 'NONE', *, *, #13290, .T. ) ;
#25393=EDGE_CURVE ( 'NONE', #9747, #6952, #15066, .T. ) ;
#25432=EDGE_LOOP ( 'NONE', ( #18634, #18729, #29605, #9193 ) ) ;
#25440=CYLINDRICAL_SURFACE ( 'NONE', #30954, 13.99999999999999822 ) ;
#25471=DIRECTION ( 'NONE',  ( 0.000000000000000000, 0.000000000000000000, -1.000000000000000000 ) ) ;
#25477=CIRCLE ( 'NONE', #33505, 9.499000000000011212 ) ;
#25481=EDGE_CURVE ( 'NONE', #741, #23024, #26816, .T. ) ;
#25538=CIRCLE ( 'NONE', #20907, 9.499000000000009436 ) ;
#25559=ORIENTED_EDGE ( 'NONE', *, *, #2029, .T. ) ;
#25579=EDGE_CURVE ( 'NONE', #34823, #19114, #32184, .T. ) ;
#25595=CARTESIAN_POINT ( 'NONE',  ( 8.000000000000007105, 0.000000000000000000, 0.000000000000000000 ) ) ;
#25644=CARTESIAN_POINT ( 'NONE',  ( 0.000000000000000000, 0.3151488735050472778, -11.27190672109269087 ) ) ;
#25674=VERTEX_POINT ( 'NONE', #10754 ) ;
#25700=MECHANICAL_DESIGN_GEOMETRIC_PRESENTATION_REPRESENTATION('',(#29113),#29143);
#25709=ORIENTED_EDGE ( 'NONE', *, *, #17176, .T. ) ;
#25711=DIRECTION ( 'NONE',  ( 0.000000000000000000, 0.000000000000000000, 1.000000000000000000 ) ) ;
#25712=DIRECTION ( 'NONE',  ( -1.000000000000000000, 0.000000000000000000, 0.000000000000000000 ) ) ;
#25713=VERTEX_POINT ( 'NONE', #32716 ) ;
#25714=CARTESIAN_POINT ( 'NONE',  ( 0.000000000000000000, -11.27190672109260028, -0.3151488735048807444 ) ) ;
#25720=CIRCLE ( 'NONE', #4450, 4.800000000000000711 ) ;
#25722=DIRECTION ( 'NONE',  ( 0.000000000000000000, 0.000000000000000000, 1.000000000000000000 ) ) ;
#25732=AXIS2_PLACEMENT_3D ( 'NONE', #16501, #5016, #24446 ) ;
#25752=ORIENTED_EDGE ( 'NONE', *, *, #11756, .F. ) ;
#25756=DIRECTION ( 'NONE',  ( -1.000000000000000000, 0.000000000000000000, 0.000000000000000000 ) ) ;
#25768=PRESENTATION_STYLE_ASSIGNMENT (( #17992 ) ) ;
#25769=ORIENTED_EDGE ( 'NONE', *, *, #25939, .T. ) ;
#25771=CARTESIAN_POINT ( 'NONE',  ( 4.000000000000003553, -9.637487275701184686, 10.15474465512046542 ) ) ;
#25776=ORIENTED_EDGE ( 'NONE', *, *, #6649, .F. ) ;
#25783=DIRECTION ( 'NONE',  ( -1.000000000000000000, 0.000000000000000000, 0.000000000000000000 ) ) ;
#25793=CARTESIAN_POINT ( 'NONE',  ( 8.000000000000007105, 9.433698091065187086, -1.111908866155128628 ) ) ;
#25837=DIRECTION ( 'NONE',  ( 1.000000000000000000, -0.000000000000000000, 0.000000000000000000 ) ) ;
#25858=ORIENTED_EDGE ( 'NONE', *, *, #1521, .F. ) ;
#25868=CYLINDRICAL_SURFACE ( 'NONE', #10083, 9.499000000000000554 ) ;
#25900=FACE_OUTER_BOUND ( 'NONE', #5297, .T. ) ;
#25939=EDGE_CURVE ( 'NONE', #16008, #3725, #30283, .T. ) ;
#25985=DIRECTION ( 'NONE',  ( -1.000000000000000000, 0.000000000000000000, 0.000000000000000000 ) ) ;
#26038=CARTESIAN_POINT ( 'NONE',  ( 4.000000000000003553, 3.268936481846174136, 13.61301047812919762 ) ) ;
#26076=CARTESIAN_POINT ( 'NONE',  ( 50.00005079999998969, 4.898587196589412829E-16, -4.000000000000000000 ) ) ;
#26078=CIRCLE ( 'NONE', #27242, 4.800000000000001599 ) ;
#26083=CARTESIAN_POINT ( 'NONE',  ( 0.000000000000000000, -9.433698091065103597, 1.111908866155073117 ) ) ;
#26090=CYLINDRICAL_SURFACE ( 'NONE', #11742, 4.800000000000000711 ) ;
#26098=CARTESIAN_POINT ( 'NONE',  ( 4.000000000000003553, -10.15474465512046542, 9.637487275701101197 ) ) ;
#26104=CARTESIAN_POINT ( 'NONE',  ( 0.000000000000000000, 1.111908866155100650, 9.433698091065117808 ) ) ;
#26124=CARTESIAN_POINT ( 'NONE',  ( 8.000000000000007105, 0.000000000000000000, 0.000000000000000000 ) ) ;
#26209=ADVANCED_FACE ( 'NONE', ( #18988 ), #21863, .T. ) ;
#26223=DIRECTION ( 'NONE',  ( 0.000000000000000000, -0.8660254037844431485, 0.4999999999999921729 ) ) ;
#26228=AXIS2_PLACEMENT_3D ( 'NONE', #14933, #1265, #17458 ) ;
#26231=VERTEX_POINT ( 'NONE', #13589 ) ;
#26235=DIRECTION ( 'NONE',  ( -1.000000000000000000, 0.000000000000000000, 0.000000000000000000 ) ) ;
#26260=CIRCLE ( 'NONE', #30851, 13.99999999999999645 ) ;
#26263=ORIENTED_EDGE ( 'NONE', *, *, #7913, .T. ) ;
#26269=ORIENTED_EDGE ( 'NONE', *, *, #20914, .T. ) ;
#26278=ORIENTED_EDGE ( 'NONE', *, *, #10722, .F. ) ;
#26297=DIRECTION ( 'NONE',  ( -1.000000000000000000, 0.000000000000000000, 0.000000000000000000 ) ) ;
#26298=DIRECTION ( 'NONE',  ( 0.000000000000000000, -0.4999999999999888978, -0.8660254037844450359 ) ) ;
#26332=ORIENTED_EDGE ( 'NONE', *, *, #22013, .T. ) ;
#26335=CIRCLE ( 'NONE', #34380, 4.800000000000004263 ) ;
#26336=ADVANCED_FACE ( 'NONE', ( #16973 ), #27981, .T. ) ;
#26361=DIRECTION ( 'NONE',  ( -1.000000000000000000, 0.000000000000000000, 0.000000000000000000 ) ) ;
#26372=DIRECTION ( 'NONE',  ( -1.000000000000000000, 0.000000000000000000, 0.000000000000000000 ) ) ;
#26417=EDGE_CURVE ( 'NONE', #17643, #22617, #19842, .T. ) ;
#26423=VERTEX_POINT ( 'NONE', #28157 ) ;
#26446=ORIENTED_EDGE ( 'NONE', *, *, #25393, .F. ) ;
#26486=DIRECTION ( 'NONE',  ( 1.000000000000000000, -0.000000000000000000, -0.000000000000000000 ) ) ;
#26497=DIRECTION ( 'NONE',  ( 0.000000000000000000, 0.000000000000000000, 1.000000000000000000 ) ) ;
#26519=ORIENTED_EDGE ( 'NONE', *, *, #6251, .F. ) ;
#26527=CARTESIAN_POINT ( 'NONE',  ( -9.999999999999994671, 0.000000000000000000, 0.000000000000000000 ) ) ;
#26531=DIRECTION ( 'NONE',  ( 0.000000000000000000, -1.000000000000000000, 0.000000000000000000 ) ) ;
#26535=VERTEX_POINT ( 'NONE', #10458 ) ;
#26568=CARTESIAN_POINT ( 'NONE',  ( 8.000000000000007105, 0.000000000000000000, 0.000000000000000000 ) ) ;
#26589=CARTESIAN_POINT ( 'NONE',  ( 0.000000000000000000, 0.000000000000000000, 0.000000000000000000 ) ) ;
#26594=EDGE_CURVE ( 'NONE', #27346, #13312, #23846, .T. ) ;
#26603=CIRCLE ( 'NONE', #20234, 4.800000000000000711 ) ;
#26604=CARTESIAN_POINT ( 'NONE',  ( 0.000000000000000000, 0.000000000000000000, 0.000000000000000000 ) ) ;
#26648=ORIENTED_EDGE ( 'NONE', *, *, #9664, .F. ) ;
#26665=ORIENTED_EDGE ( 'NONE', *, *, #1005, .F. ) ;
#26673=AXIS2_PLACEMENT_3D ( 'NONE', #18618, #5312, #35375 ) ;
#26713=CARTESIAN_POINT ( 'NONE',  ( 8.000000000000007105, -1.111908866155156161, 9.433698091065117808 ) ) ;
#26734=AXIS2_PLACEMENT_3D ( 'NONE', #9510, #23010, #20470 ) ;
#26745=VERTEX_POINT ( 'NONE', #26083 ) ;
#26750=DIRECTION ( 'NONE',  ( 0.000000000000000000, 0.000000000000000000, 1.000000000000000000 ) ) ;
#26773=CARTESIAN_POINT ( 'NONE',  ( 8.000000000000007105, -7.613867765417476008, -5.679790370316101011 ) ) ;
#26802=DIRECTION ( 'NONE',  ( -1.000000000000000000, 0.000000000000000000, 0.000000000000000000 ) ) ;
#26807=ORIENTED_EDGE ( 'NONE', *, *, #17134, .F. ) ;
#26816=CIRCLE ( 'NONE', #25083, 4.800000000000006040 ) ;
#26830=DIRECTION ( 'NONE',  ( 0.000000000000000000, 0.000000000000000000, 1.000000000000000000 ) ) ;
#26849=VERTEX_POINT ( 'NONE', #28423 ) ;
#26877=EDGE_CURVE ( 'NONE', #19237, #33648, #30944, .T. ) ;
#26883=AXIS2_PLACEMENT_3D ( 'NONE', #24576, #13242, #16084 ) ;
#26887=VERTEX_POINT ( 'NONE', #866 ) ;
#26906=ORIENTED_EDGE ( 'NONE', *, *, #14923, .T. ) ;
#26909=EDGE_CURVE ( 'NONE', #1552, #17434, #9467, .T. ) ;
#26916=ADVANCED_FACE ( 'NONE', ( #14538 ), #17596, .T. ) ;
#26926=CIRCLE ( 'NONE', #15967, 4.800000000000001599 ) ;
#26944=CARTESIAN_POINT ( 'NONE',  ( 0.000000000000000000, 3.975523202428013381, 13.42368113696675103 ) ) ;
#26960=EDGE_CURVE ( 'NONE', #9557, #2406, #29144, .T. ) ;
#26984=CARTESIAN_POINT ( 'NONE',  ( 8.000000000000007105, 0.000000000000000000, 0.000000000000000000 ) ) ;
#27003=LINE ( 'NONE', #4697, #15494 ) ;
#27016=CARTESIAN_POINT ( 'NONE',  ( 8.000000000000007105, 11.27190672109280811, 4.484851126495202678 ) ) ;
#27092=LINE ( 'NONE', #30139, #29167 ) ;
#27101=CARTESIAN_POINT ( 'NONE',  ( 4.000000000000003553, -3.975523202428068892, 13.42368113696675103 ) ) ;
#27117=EDGE_CURVE ( 'NONE', #25259, #10473, #35612, .T. ) ;
#27126=( GEOMETRIC_REPRESENTATION_CONTEXT ( 3 ) GLOBAL_UNCERTAINTY_ASSIGNED_CONTEXT ( ( #28687 ) ) GLOBAL_UNIT_ASSIGNED_CONTEXT ( ( #10148, #15712, #753 ) ) REPRESENTATION_CONTEXT ( 'NONE', 'WORKASPACE' ) );
#27163=ORIENTED_EDGE ( 'NONE', *, *, #9775, .F. ) ;
#27166=EDGE_CURVE ( 'NONE', #20656, #10643, #29032, .T. ) ;
#27242=AXIS2_PLACEMENT_3D ( 'NONE', #28292, #13896, #6144 ) ;
#27258=VERTEX_POINT ( 'NONE', #5368 ) ;
#27265=CIRCLE ( 'NONE', #19740, 4.800000000000002487 ) ;
#27267=CARTESIAN_POINT ( 'NONE',  ( 8.000000000000007105, 0.000000000000000000, 0.000000000000000000 ) ) ;
#27281=CARTESIAN_POINT ( 'NONE',  ( 8.000000000000007105, -5.363026430117032284, -9.919332006307277183 ) ) ;
#27287=CYLINDRICAL_SURFACE ( 'NONE', #21613, 13.99999999999999822 ) ;
#27288=ORIENTED_EDGE ( 'NONE', *, *, #23117, .F. ) ;
#27296=VERTEX_POINT ( 'NONE', #1023 ) ;
#27327=DIRECTION ( 'NONE',  ( -1.000000000000000000, 0.000000000000000000, 0.000000000000000000 ) ) ;
#27332=EDGE_LOOP ( 'NONE', ( #22397, #12980, #9257, #17426, #11690, #22486, #16023, #22865, #3587, #29909, #19264, #13133, #34153, #15350, #10600, #29446, #31541, #26807, #32074, #28430, #16495, #31829, #1534, #27564, #5429, #35435, #9668, #2830, #2255, #11340, #34367, #21829, #18892, #10867, #19714, #7217, #26648, #21203, #14999, #10837, #16690, #5408, #16201, #19468, #27609, #11925, #24390, #3329, #271, #9461, #31778, #16550, #7363 ) ) ;
#27346=VERTEX_POINT ( 'NONE', #14494 ) ;
#27375=EDGE_CURVE ( 'NONE', #15703, #27617, #20421, .T. ) ;
#27396=VECTOR ( 'NONE', #12843, 1000.000000000000000 ) ;
#27404=CARTESIAN_POINT ( 'NONE',  ( 0.000000000000000000, 9.604183132802424083, -1.108880290975567950 ) ) ;
#27414=VERTEX_POINT ( 'NONE', #34680 ) ;
#27447=VECTOR ( 'NONE', #15957, 1000.000000000000000 ) ;
#27457=AXIS2_PLACEMENT_3D ( 'NONE', #7689, #16317, #18500 ) ;
#27471=DIRECTION ( 'NONE',  ( -1.000000000000000000, 0.000000000000000000, 0.000000000000000000 ) ) ;
#27499=CARTESIAN_POINT ( 'NONE',  ( -9.999999999999994671, 0.000000000000000000, 0.000000000000000000 ) ) ;
#27507=DIRECTION ( 'NONE',  ( 0.000000000000000000, 0.000000000000000000, 1.000000000000000000 ) ) ;
#27513=CARTESIAN_POINT ( 'NONE',  ( 0.000000000000000000, 0.000000000000000000, 0.000000000000000000 ) ) ;
#27532=ORIENTED_EDGE ( 'NONE', *, *, #2477, .T. ) ;
#27545=DIRECTION ( 'NONE',  ( 0.000000000000000000, -0.8660254037844431485, 0.4999999999999921729 ) ) ;
#27558=AXIS2_PLACEMENT_3D ( 'NONE', #29790, #2262, #13228 ) ;
#27564=ORIENTED_EDGE ( 'NONE', *, *, #9342, .F. ) ;
#27580=ORIENTED_EDGE ( 'NONE', *, *, #8829, .F. ) ;
#27591=EDGE_CURVE ( 'NONE', #15523, #3873, #7827, .T. ) ;
#27595=ORIENTED_EDGE ( 'NONE', *, *, #4931, .T. ) ;
#27596=ORIENTED_EDGE ( 'NONE', *, *, #18972, .T. ) ;
#27600=ORIENTED_EDGE ( 'NONE', *, *, #6840, .T. ) ;
#27602=ORIENTED_EDGE ( 'NONE', *, *, #1521, .T. ) ;
#27603=ADVANCED_FACE ( 'NONE', ( #257, #24230 ), #32861, .F. ) ;
#27609=ORIENTED_EDGE ( 'NONE', *, *, #5011, .F. ) ;
#27611=DIRECTION ( 'NONE',  ( 0.000000000000000000, -0.5000000000000068834, 0.8660254037844347108 ) ) ;
#27617=VERTEX_POINT ( 'NONE', #4276 ) ;
#27649=CARTESIAN_POINT ( 'NONE',  ( 0.000000000000000000, 0.000000000000000000, 0.000000000000000000 ) ) ;
#27650=DIRECTION ( 'NONE',  ( -1.000000000000000000, 0.000000000000000000, 0.000000000000000000 ) ) ;
#27737=DIRECTION ( 'NONE',  ( -1.000000000000000000, 0.000000000000000000, 0.000000000000000000 ) ) ;
#27759=FACE_OUTER_BOUND ( 'NONE', #14149, .T. ) ;
#27769=CARTESIAN_POINT ( 'NONE',  ( 0.000000000000000000, 0.000000000000000000, 0.000000000000000000 ) ) ;
#27787=( LENGTH_UNIT ( ) NAMED_UNIT ( * ) SI_UNIT ( .MILLI., .METRE. ) );
#27830=FACE_OUTER_BOUND ( 'NONE', #34145, .T. ) ;
#27844=CARTESIAN_POINT ( 'NONE',  ( 8.000000000000007105, 0.000000000000000000, 0.000000000000000000 ) ) ;
#27873=CARTESIAN_POINT ( 'NONE',  ( 8.000000000000007105, -13.42368113696662490, -3.975523202428152381 ) ) ;
#27875=DIRECTION ( 'NONE',  ( -1.000000000000000000, 0.000000000000000000, 0.000000000000000000 ) ) ;
#27878=DIRECTION ( 'NONE',  ( 0.000000000000000000, 0.000000000000000000, -1.000000000000000000 ) ) ;
#27889=DIRECTION ( 'NONE',  ( -1.000000000000000000, 0.000000000000000000, 0.000000000000000000 ) ) ;
#27928=ORIENTED_EDGE ( 'NONE', *, *, #28005, .F. ) ;
#27942=ORIENTED_EDGE ( 'NONE', *, *, #24682, .T. ) ;
#27975=LINE ( 'NONE', #3326, #31173 ) ;
#27976=DIRECTION ( 'NONE',  ( -1.000000000000000000, 0.000000000000000000, 0.000000000000000000 ) ) ;
#27981=CYLINDRICAL_SURFACE ( 'NONE', #18582, 4.800000000000000711 ) ;
#27982=CARTESIAN_POINT ( 'NONE',  ( 4.000000000000003553, -10.15474465512033930, -9.637487275701225542 ) ) ;
#28005=EDGE_CURVE ( 'NONE', #17434, #23255, #33124, .T. ) ;
#28022=CARTESIAN_POINT ( 'NONE',  ( 0.000000000000000000, 0.000000000000000000, 0.000000000000000000 ) ) ;
#28043=DIRECTION ( 'NONE',  ( 1.000000000000000000, -0.000000000000000000, 0.000000000000000000 ) ) ;
#28044=ORIENTED_EDGE ( 'NONE', *, *, #17857, .T. ) ;
#28084=DIRECTION ( 'NONE',  ( -1.000000000000000000, 0.000000000000000000, 0.000000000000000000 ) ) ;
#28089=FACE_OUTER_BOUND ( 'NONE', #6395, .T. ) ;
#28103=AXIS2_PLACEMENT_3D ( 'NONE', #25300, #11437, #19521 ) ;
#28123=ORIENTED_EDGE ( 'NONE', *, *, #26909, .T. ) ;
#28133=SURFACE_STYLE_FILL_AREA ( #5645 ) ;
#28154=LINE ( 'NONE', #9241, #716 ) ;
#28155=EDGE_LOOP ( 'NONE', ( #4267, #3693, #13997, #30784, #17305, #26665 ) ) ;
#28157=CARTESIAN_POINT ( 'NONE',  ( 0.000000000000000000, -3.268936481846063113, -13.61301047812921183 ) ) ;
#28167=DIRECTION ( 'NONE',  ( 0.000000000000000000, 0.000000000000000000, 1.000000000000000000 ) ) ;
#28185=DIRECTION ( 'NONE',  ( -1.000000000000000000, 0.000000000000000000, 0.000000000000000000 ) ) ;
#28196=DIRECTION ( 'NONE',  ( 0.000000000000000000, 0.8660254037844362651, 0.5000000000000041078 ) ) ;
#28225=VERTEX_POINT ( 'NONE', #31122 ) ;
#28246=DIRECTION ( 'NONE',  ( -1.000000000000000000, 0.000000000000000000, 0.000000000000000000 ) ) ;
#28248=EDGE_CURVE ( 'NONE', #14077, #16923, #26260, .T. ) ;
#28284=CARTESIAN_POINT ( 'NONE',  ( 8.000000000000007105, 8.725776631572770725, -3.753907720748954180 ) ) ;
#28292=CARTESIAN_POINT ( 'NONE',  ( 0.000000000000000000, 11.27190672109280811, -0.3151488735047974776 ) ) ;
#28316=CARTESIAN_POINT ( 'NONE',  ( 8.000000000000007105, 11.27190672109271219, 0.3151488735049640111 ) ) ;
#28334=DIRECTION ( 'NONE',  ( -1.000000000000000000, 0.000000000000000000, 0.000000000000000000 ) ) ;
#28350=CYLINDRICAL_SURFACE ( 'NONE', #15437, 9.499000000000000554 ) ;
#28379=ORIENTED_EDGE ( 'NONE', *, *, #7627, .T. ) ;
#28395=ORIENTED_EDGE ( 'NONE', *, *, #15678, .T. ) ;
#28402=ORIENTED_EDGE ( 'NONE', *, *, #20227, .T. ) ;
#28423=CARTESIAN_POINT ( 'NONE',  ( 0.000000000000000000, -7.613867765417531075, 5.679790370316011305 ) ) ;
#28430=ORIENTED_EDGE ( 'NONE', *, *, #21512, .F. ) ;
#28437=ORIENTED_EDGE ( 'NONE', *, *, #23302, .T. ) ;
#28457=FILL_AREA_STYLE ('',( #28642 ) ) ;
#28465=AXIS2_PLACEMENT_3D ( 'NONE', #27513, #18857, #5881 ) ;
#28466=ORIENTED_EDGE ( 'NONE', *, *, #17176, .F. ) ;
#28492=EDGE_CURVE ( 'NONE', #23109, #6425, #6688, .T. ) ;
#28568=ORIENTED_EDGE ( 'NONE', *, *, #11800, .T. ) ;
#28570=ORIENTED_EDGE ( 'NONE', *, *, #8965, .T. ) ;
#28613=DIRECTION ( 'NONE',  ( 0.000000000000000000, 0.000000000000000000, 1.000000000000000000 ) ) ;
#28642=FILL_AREA_STYLE_COLOUR ( '', #21610 ) ;
#28659=CARTESIAN_POINT ( 'NONE',  ( 8.000000000000007105, 0.000000000000000000, 0.000000000000000000 ) ) ;
#28687=UNCERTAINTY_MEASURE_WITH_UNIT (LENGTH_MEASURE( 1.000000000000000082E-05 ), #10148, 'distance_accuracy_value', 'NONE');
#28698=EDGE_CURVE ( 'NONE', #10424, #24324, #17628, .T. ) ;
#28702=CARTESIAN_POINT ( 'NONE',  ( 0.000000000000000000, -5.679790370315976666, -7.613867765417642097 ) ) ;
#28707=CARTESIAN_POINT ( 'NONE',  ( 0.000000000000000000, -11.27190672109260028, -0.3151488735048807444 ) ) ;
#28764=DIRECTION ( 'NONE',  ( 0.000000000000000000, 0.000000000000000000, 1.000000000000000000 ) ) ;
#28788=FACE_OUTER_BOUND ( 'NONE', #11125, .T. ) ;
#28814=FACE_OUTER_BOUND ( 'NONE', #30041, .T. ) ;
#28852=DIRECTION ( 'NONE',  ( -1.000000000000000000, 0.000000000000000000, 0.000000000000000000 ) ) ;
#28861=CARTESIAN_POINT ( 'NONE',  ( 7.999999999999992895, 9.714451465470119729E-14, 1.000000000000000888 ) ) ;
#28911=CARTESIAN_POINT ( 'NONE',  ( 0.000000000000000000, 3.872983346207531596, 1.000000000000000888 ) ) ;
#28926=DIRECTION ( 'NONE',  ( -1.000000000000000000, 0.000000000000000000, 0.000000000000000000 ) ) ;
#28932=AXIS2_PLACEMENT_3D ( 'NONE', #28707, #25837, #25471 ) ;
#28959=DIRECTION ( 'NONE',  ( -1.000000000000000000, 0.000000000000000000, 0.000000000000000000 ) ) ;
#28990=DIRECTION ( 'NONE',  ( -1.000000000000000000, 0.000000000000000000, 0.000000000000000000 ) ) ;
#28994=ORIENTED_EDGE ( 'NONE', *, *, #26909, .F. ) ;
#28996=ORIENTED_EDGE ( 'NONE', *, *, #32341, .T. ) ;
#29005=DIRECTION ( 'NONE',  ( -1.000000000000000000, 0.000000000000000000, 0.000000000000000000 ) ) ;
#29016=CARTESIAN_POINT ( 'NONE',  ( 4.000000000000003553, 13.61301047812928111, 3.268936481846215880 ) ) ;
#29021=EDGE_CURVE ( 'NONE', #26745, #14077, #12481, .T. ) ;
#29032=CIRCLE ( 'NONE', #28465, 4.000000000000000000 ) ;
#29037=LINE ( 'NONE', #28861, #34984 ) ;
#29055=CYLINDRICAL_SURFACE ( 'NONE', #8813, 9.499000000000000554 ) ;
#29068=EDGE_CURVE ( 'NONE', #26887, #26849, #13091, .T. ) ;
#29069=CARTESIAN_POINT ( 'NONE',  ( 0.000000000000000000, -5.363026430117185051, 9.919332006307207905 ) ) ;
#29112=CARTESIAN_POINT ( 'NONE',  ( 8.000000000000007105, -9.433698091065020108, -1.111908866155191022 ) ) ;
#29113=STYLED_ITEM ( 'NONE', ( #25768 ), #22248 ) ;
#29116=DIRECTION ( 'NONE',  ( -1.000000000000000000, 0.000000000000000000, 0.000000000000000000 ) ) ;
#29131=CARTESIAN_POINT ( 'NONE',  ( 8.000000000000007105, -3.268936481846215880, 13.61301047812921183 ) ) ;
#29132=EDGE_CURVE ( 'NONE', #6246, #26231, #16500, .T. ) ;
#29137=EDGE_CURVE ( 'NONE', #13147, #14425, #17661, .T. ) ;
#29143=( GEOMETRIC_REPRESENTATION_CONTEXT ( 3 ) GLOBAL_UNCERTAINTY_ASSIGNED_CONTEXT ( ( #12514 ) ) GLOBAL_UNIT_ASSIGNED_CONTEXT ( ( #1096, #31519, #29185 ) ) REPRESENTATION_CONTEXT ( 'NONE', 'WORKASPACE' ) );
#29144=LINE ( 'NONE', #23732, #5472 ) ;
#29167=VECTOR ( 'NONE', #2266, 1000.000000000000000 ) ;
#29180=CARTESIAN_POINT ( 'NONE',  ( 8.000000000000007105, -7.613867765417531075, 5.679790370316011305 ) ) ;
#29185=( NAMED_UNIT ( * ) SI_UNIT ( $, .STERADIAN. ) SOLID_ANGLE_UNIT ( ) );
#29190=ORIENTED_EDGE ( 'NONE', *, *, #11651, .T. ) ;
#29225=AXIS2_PLACEMENT_3D ( 'NONE', #16726, #27737, #6111 ) ;
#29227=DIRECTION ( 'NONE',  ( -1.000000000000000000, 0.000000000000000000, 0.000000000000000000 ) ) ;
#29236=CARTESIAN_POINT ( 'NONE',  ( 0.000000000000000000, 0.000000000000000000, 0.000000000000000000 ) ) ;
#29245=DIRECTION ( 'NONE',  ( 0.000000000000000000, 0.000000000000000000, 1.000000000000000000 ) ) ;
#29253=ORIENTED_EDGE ( 'NONE', *, *, #34721, .T. ) ;
#29257=ADVANCED_BREP_SHAPE_REPRESENTATION ( '', ( #22248, #21307 ), #27126 ) ;
#29268=DIRECTION ( 'NONE',  ( 0.000000000000000000, 0.000000000000000000, 1.000000000000000000 ) ) ;
#29274=DIRECTION ( 'NONE',  ( -1.000000000000000000, 0.000000000000000000, 0.000000000000000000 ) ) ;
#29297=CIRCLE ( 'NONE', #31575, 14.00000000000000000 ) ;
#29329=VERTEX_POINT ( 'NONE', #7573 ) ;
#29330=ORIENTED_EDGE ( 'NONE', *, *, #27117, .T. ) ;
#29347=EDGE_LOOP ( 'NONE', ( #25858, #26278, #31851, #3719 ) ) ;
#29387=CARTESIAN_POINT ( 'NONE',  ( 8.000000000000007105, 0.000000000000000000, 0.000000000000000000 ) ) ;
#29398=CARTESIAN_POINT ( 'NONE',  ( 8.000000000000007105, 5.679790370316031733, 7.613867765417614564 ) ) ;
#29422=CARTESIAN_POINT ( 'NONE',  ( 8.000000000000007105, -11.27190672109268377, 0.3151488735047419665 ) ) ;
#29426=EDGE_CURVE ( 'NONE', #29329, #17886, #32040, .T. ) ;
#29428=CIRCLE ( 'NONE', #23667, 4.800000000000005151 ) ;
#29446=ORIENTED_EDGE ( 'NONE', *, *, #32159, .F. ) ;
#29473=AXIS2_PLACEMENT_3D ( 'NONE', #2658, #35599, #30017 ) ;
#29474=CARTESIAN_POINT ( 'NONE',  ( 7.999999999999992895, 0.000000000000000000, 0.000000000000000000 ) ) ;
#29482=CIRCLE ( 'NONE', #15080, 13.99999999999999645 ) ;
#29520=AXIS2_PLACEMENT_3D ( 'NONE', #19219, #19403, #15985 ) ;
#29528=ADVANCED_FACE ( 'NONE', ( #28089 ), #5769, .T. ) ;
#29532=DIRECTION ( 'NONE',  ( 0.000000000000000000, 0.000000000000000000, -1.000000000000000000 ) ) ;
#29542=LINE ( 'NONE', #12970, #16898 ) ;
#29563=DIRECTION ( 'NONE',  ( 0.000000000000000000, 0.000000000000000000, 1.000000000000000000 ) ) ;
#29566=DIRECTION ( 'NONE',  ( -1.000000000000000000, 0.000000000000000000, 0.000000000000000000 ) ) ;
#29598=ORIENTED_EDGE ( 'NONE', *, *, #35012, .T. ) ;
#29604=ORIENTED_EDGE ( 'NONE', *, *, #22875, .F. ) ;
#29605=ORIENTED_EDGE ( 'NONE', *, *, #18321, .F. ) ;
#29638=DIRECTION ( 'NONE',  ( -1.000000000000000000, 0.000000000000000000, 0.000000000000000000 ) ) ;
#29670=DIRECTION ( 'NONE',  ( -1.000000000000000000, 0.000000000000000000, 0.000000000000000000 ) ) ;
#29722=ORIENTED_EDGE ( 'NONE', *, *, #35542, .T. ) ;
#29739=ORIENTED_EDGE ( 'NONE', *, *, #29962, .F. ) ;
#29753=AXIS2_PLACEMENT_3D ( 'NONE', #25142, #22589, #28196 ) ;
#29790=CARTESIAN_POINT ( 'NONE',  ( 8.000000000000007105, -0.3151488735047419665, 11.27190672109269798 ) ) ;
#29830=VERTEX_POINT ( 'NONE', #31839 ) ;
#29833=FACE_BOUND ( 'NONE', #28155, .T. ) ;
#29839=AXIS2_PLACEMENT_3D ( 'NONE', #13492, #1984, #29532 ) ;
#29843=DIRECTION ( 'NONE',  ( -1.000000000000000000, 0.000000000000000000, 0.000000000000000000 ) ) ;
#29856=DIRECTION ( 'NONE',  ( 0.000000000000000000, -1.000000000000000000, -1.048062100069320848E-14 ) ) ;
#29902=DIRECTION ( 'NONE',  ( -1.000000000000000000, 0.000000000000000000, 0.000000000000000000 ) ) ;
#29909=ORIENTED_EDGE ( 'NONE', *, *, #6858, .F. ) ;
#29913=ORIENTED_EDGE ( 'NONE', *, *, #28698, .T. ) ;
#29930=CARTESIAN_POINT ( 'NONE',  ( 8.000000000000007105, 10.15474465512070168, -9.637487275700989287 ) ) ;
#29949=DIRECTION ( 'NONE',  ( 0.000000000000000000, 0.000000000000000000, 1.000000000000000000 ) ) ;
#29957=ORIENTED_EDGE ( 'NONE', *, *, #9748, .T. ) ;
#29962=EDGE_CURVE ( 'NONE', #26423, #25092, #24388, .T. ) ;
#29968=EDGE_CURVE ( 'NONE', #10771, #18371, #3033, .T. ) ;
#29982=DIRECTION ( 'NONE',  ( 0.000000000000000000, 0.000000000000000000, 1.000000000000000000 ) ) ;
#30002=( GEOMETRIC_REPRESENTATION_CONTEXT ( 3 ) GLOBAL_UNCERTAINTY_ASSIGNED_CONTEXT ( ( #14977 ) ) GLOBAL_UNIT_ASSIGNED_CONTEXT ( ( #27787, #14075, #55 ) ) REPRESENTATION_CONTEXT ( 'NONE', 'WORKASPACE' ) );
#30017=DIRECTION ( 'NONE',  ( 0.000000000000000000, 1.000000000000000000, 3.614007241618346010E-15 ) ) ;
#30023=CARTESIAN_POINT ( 'NONE',  ( 0.000000000000000000, -11.27190672109268377, 0.3151488735047419665 ) ) ;
#30031=CARTESIAN_POINT ( 'NONE',  ( 8.000000000000007105, -5.908880290975456973, -9.604183132802479150 ) ) ;
#30032=DIRECTION ( 'NONE',  ( 1.000000000000000000, -0.000000000000000000, 0.000000000000000000 ) ) ;
#30041=EDGE_LOOP ( 'NONE', ( #9865, #30048, #20927, #12585 ) ) ;
#30044=LINE ( 'NONE', #19396, #6211 ) ;
#30048=ORIENTED_EDGE ( 'NONE', *, *, #17857, .F. ) ;
#30065=CARTESIAN_POINT ( 'NONE',  ( 0.000000000000000000, 5.363026430117226795, 9.919332006307262972 ) ) ;
#30076=DIRECTION ( 'NONE',  ( -1.000000000000000000, 0.000000000000000000, 0.000000000000000000 ) ) ;
#30082=VECTOR ( 'NONE', #11950, 1000.000000000000000 ) ;
#30084=ORIENTED_EDGE ( 'NONE', *, *, #18799, .F. ) ;
#30088=ORIENTED_EDGE ( 'NONE', *, *, #35025, .T. ) ;
#30104=CARTESIAN_POINT ( 'NONE',  ( 50.00005079999998969, 0.000000000000000000, 0.000000000000000000 ) ) ;
#30105=ORIENTED_EDGE ( 'NONE', *, *, #1005, .T. ) ;
#30113=AXIS2_PLACEMENT_3D ( 'NONE', #8562, #16483, #19533 ) ;
#30116=ADVANCED_FACE ( 'NONE', ( #3732 ), #14685, .T. ) ;
#30139=CARTESIAN_POINT ( 'NONE',  ( 7.999999999999992895, 0.000000000000000000, -1.000000000000000888 ) ) ;
#30152=FACE_OUTER_BOUND ( 'NONE', #1293, .T. ) ;
#30153=ORIENTED_EDGE ( 'NONE', *, *, #631, .F. ) ;
#30162=FACE_OUTER_BOUND ( 'NONE', #4674, .T. ) ;
#30165=FACE_OUTER_BOUND ( 'NONE', #19541, .T. ) ;
#30166=AXIS2_PLACEMENT_3D ( 'NONE', #16352, #32408, #35473 ) ;
#30193=CARTESIAN_POINT ( 'NONE',  ( 0.000000000000000000, -3.753907720749058541, 8.725776631572749409 ) ) ;
#30206=VECTOR ( 'NONE', #30627, 1000.000000000000000 ) ;
#30233=CARTESIAN_POINT ( 'NONE',  ( 0.000000000000000000, 13.61301047812926690, 3.268936481846202113 ) ) ;
#30259=ORIENTED_EDGE ( 'NONE', *, *, #25481, .T. ) ;
#30271=AXIS2_PLACEMENT_3D ( 'NONE', #726, #25049, #21983 ) ;
#30283=CIRCLE ( 'NONE', #34314, 4.800000000000000711 ) ;
#30289=DIRECTION ( 'NONE',  ( 0.000000000000000000, 0.000000000000000000, -1.000000000000000000 ) ) ;
#30304=EDGE_LOOP ( 'NONE', ( #30524, #22898, #24412, #7747 ) ) ;
#30305=ORIENTED_EDGE ( 'NONE', *, *, #26594, .T. ) ;
#30314=CARTESIAN_POINT ( 'NONE',  ( -9.999999999999994671, 0.000000000000000000, 0.000000000000000000 ) ) ;
#30345=CARTESIAN_POINT ( 'NONE',  ( 8.000000000000007105, 1.111908866155322695, -9.433698091065103597 ) ) ;
#30433=DIRECTION ( 'NONE',  ( 0.000000000000000000, -0.8660254037844431485, 0.4999999999999922284 ) ) ;
#30524=ORIENTED_EDGE ( 'NONE', *, *, #31241, .F. ) ;
#30526=CARTESIAN_POINT ( 'NONE',  ( 8.000000000000007105, -8.725776631572617958, -3.753907720749127819 ) ) ;
#30558=DIRECTION ( 'NONE',  ( -1.000000000000000000, 0.000000000000000000, 0.000000000000000000 ) ) ;
#30562=CARTESIAN_POINT ( 'NONE',  ( 0.000000000000000000, 0.000000000000000000, 0.000000000000000000 ) ) ;
#30565=CARTESIAN_POINT ( 'NONE',  ( 8.000000000000007105, -0.3151488735047419665, 11.27190672109269798 ) ) ;
#30596=CARTESIAN_POINT ( 'NONE',  ( 0.000000000000000000, -7.613867765417476008, -5.679790370316101011 ) ) ;
#30626=CARTESIAN_POINT ( 'NONE',  ( 0.000000000000000000, 10.15474465512060398, 9.637487275701170475 ) ) ;
#30627=DIRECTION ( 'NONE',  ( 1.000000000000000000, -0.000000000000000000, -0.000000000000000000 ) ) ;
#30628=ORIENTED_EDGE ( 'NONE', *, *, #29068, .T. ) ;
#30652=CARTESIAN_POINT ( 'NONE',  ( 8.000000000000007105, -3.753907720749058541, 8.725776631572749409 ) ) ;
#30668=DIRECTION ( 'NONE',  ( 0.000000000000000000, 0.000000000000000000, -1.000000000000000000 ) ) ;
#30673=EDGE_CURVE ( 'NONE', #3956, #32057, #6509, .T. ) ;
#30682=LINE ( 'NONE', #17149, #24894 ) ;
#30702=ORIENTED_EDGE ( 'NONE', *, *, #29132, .F. ) ;
#30703=DIRECTION ( 'NONE',  ( -1.000000000000000000, 0.000000000000000000, 0.000000000000000000 ) ) ;
#30783=ORIENTED_EDGE ( 'NONE', *, *, #27166, .F. ) ;
#30784=ORIENTED_EDGE ( 'NONE', *, *, #33672, .F. ) ;
#30806=EDGE_CURVE ( 'NONE', #33648, #28225, #12694, .T. ) ;
#30828=ORIENTED_EDGE ( 'NONE', *, *, #13890, .T. ) ;
#30849=DIRECTION ( 'NONE',  ( -1.000000000000000000, 0.000000000000000000, 0.000000000000000000 ) ) ;
#30851=AXIS2_PLACEMENT_3D ( 'NONE', #19931, #28246, #20643 ) ;
#30907=VECTOR ( 'NONE', #11, 1000.000000000000000 ) ;
#30924=CIRCLE ( 'NONE', #19438, 4.800000000000003375 ) ;
#30933=PLANE ( 'NONE',  #7672 ) ;
#30944=LINE ( 'NONE', #25378, #24998 ) ;
#30947=ORIENTED_EDGE ( 'NONE', *, *, #35085, .T. ) ;
#30954=AXIS2_PLACEMENT_3D ( 'NONE', #30314, #25077, #5651 ) ;
#30965=EDGE_CURVE ( 'NONE', #15523, #27258, #15542, .T. ) ;
#30971=CIRCLE ( 'NONE', #28103, 14.00000000000000000 ) ;
#31005=AXIS2_PLACEMENT_3D ( 'NONE', #28316, #6517, #19491 ) ;
#31013=VECTOR ( 'NONE', #25756, 1000.000000000000000 ) ;
#31034=PRODUCT_DEFINITION_FORMATION_WITH_SPECIFIED_SOURCE ( 'ANY', '', #12395, .NOT_KNOWN. ) ;
#31085=VERTEX_POINT ( 'NONE', #33137 ) ;
#31110=DIRECTION ( 'NONE',  ( -1.000000000000000000, 0.000000000000000000, 0.000000000000000000 ) ) ;
#31122=CARTESIAN_POINT ( 'NONE',  ( 0.000000000000000000, -10.15474465512038194, -9.637487275701211331 ) ) ;
#31130=CARTESIAN_POINT ( 'NONE',  ( 8.000000000000007105, 0.000000000000000000, 0.000000000000000000 ) ) ;
#31143=EDGE_LOOP ( 'NONE', ( #13565, #11291, #22362, #25769 ) ) ;
#31150=CARTESIAN_POINT ( 'NONE',  ( 8.000000000000007105, 0.000000000000000000, 0.000000000000000000 ) ) ;
#31173=VECTOR ( 'NONE', #30849, 1000.000000000000000 ) ;
#31178=CIRCLE ( 'NONE', #29473, 4.800000000000002487 ) ;
#31192=DIRECTION ( 'NONE',  ( 0.000000000000000000, -6.994405055138476738E-15, 1.000000000000000000 ) ) ;
#31196=DIRECTION ( 'NONE',  ( -1.000000000000000000, 0.000000000000000000, 0.000000000000000000 ) ) ;
#31202=DIRECTION ( 'NONE',  ( 0.000000000000000000, 0.000000000000000000, -1.000000000000000000 ) ) ;
#31209=CARTESIAN_POINT ( 'NONE',  ( 0.000000000000000000, 0.000000000000000000, 0.000000000000000000 ) ) ;
#31230=ADVANCED_FACE ( 'NONE', ( #34388 ), #34200, .T. ) ;
#31241=EDGE_CURVE ( 'NONE', #6425, #16937, #6468, .T. ) ;
#31253=FACE_OUTER_BOUND ( 'NONE', #15207, .T. ) ;
#31292=LINE ( 'NONE', #33454, #988 ) ;
#31302=ORIENTED_EDGE ( 'NONE', *, *, #9748, .F. ) ;
#31318=EDGE_LOOP ( 'NONE', ( #7017, #23307, #11691, #16676 ) ) ;
#31349=DIRECTION ( 'NONE',  ( -1.000000000000000000, 0.000000000000000000, 0.000000000000000000 ) ) ;
#31356=ORIENTED_EDGE ( 'NONE', *, *, #2075, .T. ) ;
#31384=AXIS2_PLACEMENT_3D ( 'NONE', #27769, #19630, #5281 ) ;
#31385=DIRECTION ( 'NONE',  ( 1.000000000000000000, -0.000000000000000000, 0.000000000000000000 ) ) ;
#31432=CARTESIAN_POINT ( 'NONE',  ( 8.000000000000007105, -13.42368113696669418, 3.975523202427999614 ) ) ;
#31472=DIRECTION ( 'NONE',  ( -1.000000000000000000, 0.000000000000000000, 0.000000000000000000 ) ) ;
#31474=AXIS2_PLACEMENT_3D ( 'NONE', #22920, #28334, #11589 ) ;
#31491=ORIENTED_EDGE ( 'NONE', *, *, #33524, .F. ) ;
#31494=CIRCLE ( 'NONE', #17100, 9.499000000000004107 ) ;
#31512=ADVANCED_FACE ( 'NONE', ( #14174 ), #19398, .T. ) ;
#31519=( NAMED_UNIT ( * ) PLANE_ANGLE_UNIT ( ) SI_UNIT ( $, .RADIAN. ) );
#31522=CARTESIAN_POINT ( 'NONE',  ( 8.000000000000007105, 9.604183132802424083, -5.908880290975567995 ) ) ;
#31526=EDGE_CURVE ( 'NONE', #34823, #24024, #21930, .T. ) ;
#31533=EDGE_CURVE ( 'NONE', #17480, #33223, #29428, .T. ) ;
#31541=ORIENTED_EDGE ( 'NONE', *, *, #28698, .F. ) ;
#31563=DIRECTION ( 'NONE',  ( 0.000000000000000000, -0.8660254037844431485, 0.4999999999999922284 ) ) ;
#31573=DIRECTION ( 'NONE',  ( 0.000000000000000000, 0.000000000000000000, -1.000000000000000000 ) ) ;
#31575=AXIS2_PLACEMENT_3D ( 'NONE', #23256, #34252, #6701 ) ;
#31671=VECTOR ( 'NONE', #34243, 1000.000000000000000 ) ;
#31697=CYLINDRICAL_SURFACE ( 'NONE', #15008, 9.499000000000000554 ) ;
#31720=EDGE_CURVE ( 'NONE', #15703, #17480, #19079, .T. ) ;
#31756=ORIENTED_EDGE ( 'NONE', *, *, #22875, .T. ) ;
#31760=DIRECTION ( 'NONE',  ( 0.000000000000000000, 0.000000000000000000, 1.000000000000000000 ) ) ;
#31769=ADVANCED_FACE ( 'NONE', ( #23705 ), #23891, .T. ) ;
#31778=ORIENTED_EDGE ( 'NONE', *, *, #7460, .F. ) ;
#31783=ORIENTED_EDGE ( 'NONE', *, *, #8625, .T. ) ;
#31808=ORIENTED_EDGE ( 'NONE', *, *, #31533, .T. ) ;
#31829=ORIENTED_EDGE ( 'NONE', *, *, #17629, .F. ) ;
#31839=CARTESIAN_POINT ( 'NONE',  ( 8.000000000000007105, -3.268936481846063113, -13.61301047812921183 ) ) ;
#31847=ADVANCED_FACE ( 'NONE', ( #2121 ), #1748, .T. ) ;
#31851=ORIENTED_EDGE ( 'NONE', *, *, #1316, .T. ) ;
#31865=DIRECTION ( 'NONE',  ( 1.000000000000000000, -0.000000000000000000, -0.000000000000000000 ) ) ;
#31875=AXIS2_PLACEMENT_3D ( 'NONE', #30065, #5406, #4875 ) ;
#31903=AXIS2_PLACEMENT_3D ( 'NONE', #11850, #3958, #22832 ) ;
#31906=LINE ( 'NONE', #20906, #32475 ) ;
#31907=EDGE_LOOP ( 'NONE', ( #28466, #32512, #10498, #29190 ) ) ;
#31924=CYLINDRICAL_SURFACE ( 'NONE', #23798, 4.800000000000000711 ) ;
#31935=ADVANCED_FACE ( 'NONE', ( #32510, #29833 ), #5172, .F. ) ;
#31939=DIRECTION ( 'NONE',  ( -1.000000000000000000, 0.000000000000000000, 0.000000000000000000 ) ) ;
#31950=EDGE_LOOP ( 'NONE', ( #16290, #343, #4492, #6381 ) ) ;
#31953=FACE_OUTER_BOUND ( 'NONE', #18090, .T. ) ;
#31978=VERTEX_POINT ( 'NONE', #22236 ) ;
#31983=EDGE_CURVE ( 'NONE', #33223, #1657, #32321, .T. ) ;
#31988=ORIENTED_EDGE ( 'NONE', *, *, #29968, .T. ) ;
#32007=AXIS2_PLACEMENT_3D ( 'NONE', #26124, #27327, #16138 ) ;
#32018=AXIS2_PLACEMENT_3D ( 'NONE', #2589, #13381, #35351 ) ;
#32023=AXIS2_PLACEMENT_3D ( 'NONE', #30023, #33071, #19536 ) ;
#32040=CIRCLE ( 'NONE', #15359, 4.800000000000003375 ) ;
#32045=CARTESIAN_POINT ( 'NONE',  ( 0.000000000000000000, 0.3151488735048668666, 11.27190672109269798 ) ) ;
#32057=VERTEX_POINT ( 'NONE', #3172 ) ;
#32060=AXIS2_PLACEMENT_3D ( 'NONE', #11107, #24434, #21898 ) ;
#32062=ORIENTED_EDGE ( 'NONE', *, *, #19863, .F. ) ;
#32074=ORIENTED_EDGE ( 'NONE', *, *, #25481, .F. ) ;
#32077=CIRCLE ( 'NONE', #21134, 4.800000000000004263 ) ;
#32084=ORIENTED_EDGE ( 'NONE', *, *, #24670, .T. ) ;
#32087=VECTOR ( 'NONE', #2234, 1000.000000000000000 ) ;
#32094=LINE ( 'NONE', #2230, #8409 ) ;
#32112=FACE_OUTER_BOUND ( 'NONE', #11063, .T. ) ;
#32113=EDGE_LOOP ( 'NONE', ( #35315, #1834, #3069, #25246 ) ) ;
#32119=ORIENTED_EDGE ( 'NONE', *, *, #13452, .F. ) ;
#32121=VECTOR ( 'NONE', #35550, 1000.000000000000000 ) ;
#32131=CARTESIAN_POINT ( 'NONE',  ( 0.000000000000000000, -0.3151488735046864553, -11.27190672109269798 ) ) ;
#32150=CARTESIAN_POINT ( 'NONE',  ( -9.999999999999994671, 0.000000000000000000, 0.000000000000000000 ) ) ;
#32159=EDGE_CURVE ( 'NONE', #24324, #26535, #2452, .T. ) ;
#32184=LINE ( 'NONE', #26076, #949 ) ;
#32216=CARTESIAN_POINT ( 'NONE',  ( 0.000000000000000000, 0.000000000000000000, 9.499000000000000554 ) ) ;
#32240=ORIENTED_EDGE ( 'NONE', *, *, #12153, .F. ) ;
#32265=EDGE_CURVE ( 'NONE', #26231, #20005, #26603, .T. ) ;
#32281=DIRECTION ( 'NONE',  ( -1.000000000000000000, 0.000000000000000000, -0.000000000000000000 ) ) ;
#32286=ORIENTED_EDGE ( 'NONE', *, *, #12416, .T. ) ;
#32301=EDGE_CURVE ( 'NONE', #21336, #7400, #13050, .T. ) ;
#32317=DIRECTION ( 'NONE',  ( 0.000000000000000000, 0.000000000000000000, 1.000000000000000000 ) ) ;
#32321=CIRCLE ( 'NONE', #16783, 9.499000000000009436 ) ;
#32338=CARTESIAN_POINT ( 'NONE',  ( 8.000000000000007105, -11.27190672109260028, -0.3151488735048807444 ) ) ;
#32341=EDGE_CURVE ( 'NONE', #16937, #33676, #29482, .T. ) ;
#32348=DIRECTION ( 'NONE',  ( 0.000000000000000000, 0.000000000000000000, 1.000000000000000000 ) ) ;
#32349=DIRECTION ( 'NONE',  ( -1.000000000000000000, 0.000000000000000000, 0.000000000000000000 ) ) ;
#32353=EDGE_CURVE ( 'NONE', #20425, #577, #24872, .T. ) ;
#32359=DIRECTION ( 'NONE',  ( -1.000000000000000000, 0.000000000000000000, 0.000000000000000000 ) ) ;
#32378=PRODUCT_DEFINITION ( 'UNKNOWN', '', #31034, #24907 ) ;
#32387=EDGE_CURVE ( 'NONE', #26849, #16937, #721, .T. ) ;
#32408=DIRECTION ( 'NONE',  ( -1.000000000000000000, 0.000000000000000000, 0.000000000000000000 ) ) ;
#32422=CIRCLE ( 'NONE', #35318, 9.499000000000009436 ) ;
#32430=ORIENTED_EDGE ( 'NONE', *, *, #15157, .T. ) ;
#32462=EDGE_LOOP ( 'NONE', ( #35342, #10292, #6081, #27163 ) ) ;
#32475=VECTOR ( 'NONE', #35165, 1000.000000000000000 ) ;
#32491=DIRECTION ( 'NONE',  ( 0.000000000000000000, 0.000000000000000000, -1.000000000000000000 ) ) ;
#32510=FACE_OUTER_BOUND ( 'NONE', #27332, .T. ) ;
#32512=ORIENTED_EDGE ( 'NONE', *, *, #15695, .F. ) ;
#32540=CIRCLE ( 'NONE', #16436, 9.499000000000000554 ) ;
#32661=EDGE_CURVE ( 'NONE', #23024, #14077, #12240, .T. ) ;
#32675=ORIENTED_EDGE ( 'NONE', *, *, #35542, .F. ) ;
#32688=DIRECTION ( 'NONE',  ( 0.000000000000000000, 0.000000000000000000, 1.000000000000000000 ) ) ;
#32689=ORIENTED_EDGE ( 'NONE', *, *, #7913, .F. ) ;
#32715=DIRECTION ( 'NONE',  ( -1.000000000000000000, 0.000000000000000000, 0.000000000000000000 ) ) ;
#32716=CARTESIAN_POINT ( 'NONE',  ( 0.000000000000000000, -9.637487275700962641, -10.15474465512060398 ) ) ;
#32728=ORIENTED_EDGE ( 'NONE', *, *, #3535, .F. ) ;
#32803=CARTESIAN_POINT ( 'NONE',  ( 4.000000000000003553, -3.268936481846215880, 13.61301047812921183 ) ) ;
#32807=DIRECTION ( 'NONE',  ( -1.000000000000000000, 0.000000000000000000, 0.000000000000000000 ) ) ;
#32829=EDGE_LOOP ( 'NONE', ( #7049, #13373, #14333, #22984 ) ) ;
#32857=CARTESIAN_POINT ( 'NONE',  ( 0.000000000000000000, -9.433698091065020108, -1.111908866155191022 ) ) ;
#32861=PLANE ( 'NONE',  #1482 ) ;
#32868=ORIENTED_EDGE ( 'NONE', *, *, #4850, .F. ) ;
#32919=CARTESIAN_POINT ( 'NONE',  ( 8.000000000000007105, 0.000000000000000000, 0.000000000000000000 ) ) ;
#32920=ORIENTED_EDGE ( 'NONE', *, *, #32661, .F. ) ;
#32957=ORIENTED_EDGE ( 'NONE', *, *, #3009, .T. ) ;
#32981=DIRECTION ( 'NONE',  ( 0.000000000000000000, 0.000000000000000000, 1.000000000000000000 ) ) ;
#32987=DIRECTION ( 'NONE',  ( 0.000000000000000000, 0.000000000000000000, -1.000000000000000000 ) ) ;
#32995=DIRECTION ( 'NONE',  ( 0.000000000000000000, 0.000000000000000000, 1.000000000000000000 ) ) ;
#32996=ORIENTED_EDGE ( 'NONE', *, *, #27166, .T. ) ;
#33050=ORIENTED_EDGE ( 'NONE', *, *, #18972, .F. ) ;
#33071=DIRECTION ( 'NONE',  ( -1.000000000000000000, 0.000000000000000000, 0.000000000000000000 ) ) ;
#33097=DIRECTION ( 'NONE',  ( -1.000000000000000000, 0.000000000000000000, 0.000000000000000000 ) ) ;
#33108=DIRECTION ( 'NONE',  ( 0.000000000000000000, 0.000000000000000000, -1.000000000000000000 ) ) ;
#33114=DIRECTION ( 'NONE',  ( 1.000000000000000000, -0.000000000000000000, 0.000000000000000000 ) ) ;
#33124=CIRCLE ( 'NONE', #35442, 9.499000000000004107 ) ;
#33137=CARTESIAN_POINT ( 'NONE',  ( 0.000000000000000000, -3.268936481846215880, 13.61301047812921183 ) ) ;
#33162=DIRECTION ( 'NONE',  ( -1.000000000000000000, 0.000000000000000000, 0.000000000000000000 ) ) ;
#33165=DIRECTION ( 'NONE',  ( 0.000000000000000000, 0.8660254037844362651, 0.5000000000000042188 ) ) ;
#33223=VERTEX_POINT ( 'NONE', #10724 ) ;
#33265=VERTEX_POINT ( 'NONE', #6202 ) ;
#33271=DIRECTION ( 'NONE',  ( 0.000000000000000000, 0.000000000000000000, 1.000000000000000000 ) ) ;
#33305=ORIENTED_EDGE ( 'NONE', *, *, #11800, .F. ) ;
#33344=VERTEX_POINT ( 'NONE', #16985 ) ;
#33364=AXIS2_PLACEMENT_3D ( 'NONE', #3886, #15183, #34119 ) ;
#33365=DIRECTION ( 'NONE',  ( 1.000000000000000000, -0.000000000000000000, 0.000000000000000000 ) ) ;
#33411=DIRECTION ( 'NONE',  ( -1.000000000000000000, 0.000000000000000000, 0.000000000000000000 ) ) ;
#33423=CYLINDRICAL_SURFACE ( 'NONE', #18831, 4.800000000000000711 ) ;
#33439=DIRECTION ( 'NONE',  ( 0.000000000000000000, 0.000000000000000000, 1.000000000000000000 ) ) ;
#33452=DIRECTION ( 'NONE',  ( 0.000000000000000000, -1.000000000000000000, 0.000000000000000000 ) ) ;
#33454=CARTESIAN_POINT ( 'NONE',  ( 8.000000000000007105, 7.613867765417711375, -5.679790370315948245 ) ) ;
#33474=ADVANCED_FACE ( 'NONE', ( #8093 ), #10632, .T. ) ;
#33480=EDGE_CURVE ( 'NONE', #27296, #13147, #32077, .T. ) ;
#33484=AXIS2_PLACEMENT_3D ( 'NONE', #18982, #10706, #7999 ) ;
#33493=AXIS2_PLACEMENT_3D ( 'NONE', #9798, #26372, #1705 ) ;
#33500=ORIENTED_EDGE ( 'NONE', *, *, #10998, .T. ) ;
#33505=AXIS2_PLACEMENT_3D ( 'NONE', #10064, #6830, #12239 ) ;
#33519=AXIS2_PLACEMENT_3D ( 'NONE', #31150, #35120, #26830 ) ;
#33524=EDGE_CURVE ( 'NONE', #22087, #18383, #11159, .T. ) ;
#33550=DIRECTION ( 'NONE',  ( -1.000000000000000000, 0.000000000000000000, 0.000000000000000000 ) ) ;
#33567=DIRECTION ( 'NONE',  ( -1.000000000000000000, 0.000000000000000000, 0.000000000000000000 ) ) ;
#33587=AXIS2_PLACEMENT_3D ( 'NONE', #31522, #6845, #7558 ) ;
#33626=CIRCLE ( 'NONE', #34809, 14.00000000000000000 ) ;
#33648=VERTEX_POINT ( 'NONE', #30596 ) ;
#33672=EDGE_CURVE ( 'NONE', #31978, #10012, #5079, .T. ) ;
#33676=VERTEX_POINT ( 'NONE', #22647 ) ;
#33682=CARTESIAN_POINT ( 'NONE',  ( 8.000000000000007105, 0.000000000000000000, 9.499000000000000554 ) ) ;
#33701=ORIENTED_EDGE ( 'NONE', *, *, #33480, .T. ) ;
#33716=EDGE_CURVE ( 'NONE', #24903, #33265, #7935, .T. ) ;
#33761=EDGE_CURVE ( 'NONE', #16526, #24903, #26926, .T. ) ;
#33817=CYLINDRICAL_SURFACE ( 'NONE', #10556, 4.800000000000000711 ) ;
#33854=CARTESIAN_POINT ( 'NONE',  ( 0.000000000000000000, 13.42368113696687537, -3.975523202427861058 ) ) ;
#33907=CARTESIAN_POINT ( 'NONE',  ( 0.000000000000000000, 3.268936481846368203, -13.61301047812914256 ) ) ;
#33956=DIRECTION ( 'NONE',  ( 0.000000000000000000, 0.000000000000000000, -1.000000000000000000 ) ) ;
#33959=DIRECTION ( 'NONE',  ( -1.000000000000000000, 0.000000000000000000, 0.000000000000000000 ) ) ;
#33982=ADVANCED_FACE ( 'NONE', ( #4842 ), #7527, .T. ) ;
#33990=ORIENTED_EDGE ( 'NONE', *, *, #4525, .T. ) ;
#33991=DIRECTION ( 'NONE',  ( 0.000000000000000000, 0.000000000000000000, -1.000000000000000000 ) ) ;
#33993=CARTESIAN_POINT ( 'NONE',  ( 0.000000000000000000, 0.000000000000000000, 0.000000000000000000 ) ) ;
#34034=CARTESIAN_POINT ( 'NONE',  ( 0.000000000000000000, 9.604183132802424083, -5.908880290975567995 ) ) ;
#34085=CARTESIAN_POINT ( 'NONE',  ( 8.000000000000007105, -11.27190672109260028, 4.484851126495120077 ) ) ;
#34119=DIRECTION ( 'NONE',  ( 0.000000000000000000, 0.000000000000000000, 1.000000000000000000 ) ) ;
#34145=EDGE_LOOP ( 'NONE', ( #15645, #2744, #8193, #30259 ) ) ;
#34153=ORIENTED_EDGE ( 'NONE', *, *, #13450, .F. ) ;
#34159=DIRECTION ( 'NONE',  ( 0.000000000000000000, 0.000000000000000000, 1.000000000000000000 ) ) ;
#34200=CYLINDRICAL_SURFACE ( 'NONE', #3523, 13.99999999999999822 ) ;
#34202=VERTEX_POINT ( 'NONE', #4269 ) ;
#34212=DIRECTION ( 'NONE',  ( -1.000000000000000000, 0.000000000000000000, 0.000000000000000000 ) ) ;
#34229=ORIENTED_EDGE ( 'NONE', *, *, #22013, .F. ) ;
#34233=CARTESIAN_POINT ( 'NONE',  ( 8.000000000000007105, 0.000000000000000000, 0.000000000000000000 ) ) ;
#34237=CARTESIAN_POINT ( 'NONE',  ( 4.000000000000003553, 13.61301047812919052, -3.268936481846215880 ) ) ;
#34243=DIRECTION ( 'NONE',  ( 1.000000000000000000, -0.000000000000000000, -0.000000000000000000 ) ) ;
#34252=DIRECTION ( 'NONE',  ( -1.000000000000000000, 0.000000000000000000, 0.000000000000000000 ) ) ;
#34277=ORIENTED_EDGE ( 'NONE', *, *, #3094, .T. ) ;
#34296=AXIS2_PLACEMENT_3D ( 'NONE', #2584, #11195, #33165 ) ;
#34314=AXIS2_PLACEMENT_3D ( 'NONE', #11993, #3713, #33956 ) ;
#34345=ADVANCED_FACE ( 'NONE', ( #30165 ), #34868, .T. ) ;
#34363=DIRECTION ( 'NONE',  ( -1.000000000000000000, 0.000000000000000000, 0.000000000000000000 ) ) ;
#34367=ORIENTED_EDGE ( 'NONE', *, *, #13903, .F. ) ;
#34380=AXIS2_PLACEMENT_3D ( 'NONE', #20369, #15511, #31563 ) ;
#34388=FACE_OUTER_BOUND ( 'NONE', #25215, .T. ) ;
#34429=LINE ( 'NONE', #34237, #5585 ) ;
#34465=ORIENTED_EDGE ( 'NONE', *, *, #35085, .F. ) ;
#34517=AXIS2_PLACEMENT_3D ( 'NONE', #17550, #14860, #1367 ) ;
#34519=DIRECTION ( 'NONE',  ( -1.000000000000000000, 0.000000000000000000, 0.000000000000000000 ) ) ;
#34532=CARTESIAN_POINT ( 'NONE',  ( 8.000000000000007105, 5.363026430117226795, 9.919332006307262972 ) ) ;
#34544=AXIS2_PLACEMENT_3D ( 'NONE', #29387, #29566, #8984 ) ;
#34551=CARTESIAN_POINT ( 'NONE',  ( 8.000000000000007105, 11.27190672109280811, -0.3151488735047974776 ) ) ;
#34611=ORIENTED_EDGE ( 'NONE', *, *, #16312, .T. ) ;
#34618=DIRECTION ( 'NONE',  ( 0.000000000000000000, -6.866613759074851423E-15, 1.000000000000000000 ) ) ;
#34623=CARTESIAN_POINT ( 'NONE',  ( 7.999999999999992895, 5.400000000000098943, 1.000000000000000888 ) ) ;
#34636=DIRECTION ( 'NONE',  ( -1.000000000000000000, 0.000000000000000000, 0.000000000000000000 ) ) ;
#34639=LINE ( 'NONE', #18594, #12483 ) ;
#34644=FACE_OUTER_BOUND ( 'NONE', #34883, .T. ) ;
#34680=CARTESIAN_POINT ( 'NONE',  ( 8.000000000000007105, -13.61301047812905907, -3.268936481846313136 ) ) ;
#34682=ORIENTED_EDGE ( 'NONE', *, *, #4265, .T. ) ;
#34713=CARTESIAN_POINT ( 'NONE',  ( 8.000000000000007105, -9.637487275700962641, -10.15474465512060398 ) ) ;
#34721=EDGE_CURVE ( 'NONE', #16923, #10424, #7257, .T. ) ;
#34796=EDGE_CURVE ( 'NONE', #3677, #8987, #21054, .T. ) ;
#34809=AXIS2_PLACEMENT_3D ( 'NONE', #2928, #24877, #13887 ) ;
#34815=DIRECTION ( 'NONE',  ( -1.000000000000000000, 0.000000000000000000, 0.000000000000000000 ) ) ;
#34823=VERTEX_POINT ( 'NONE', #16055 ) ;
#34856=CARTESIAN_POINT ( 'NONE',  ( 8.000000000000007105, 0.3151488735048668666, 11.27190672109269798 ) ) ;
#34868=CYLINDRICAL_SURFACE ( 'NONE', #3888, 4.800000000000000711 ) ;
#34876=ORIENTED_EDGE ( 'NONE', *, *, #30965, .T. ) ;
#34883=EDGE_LOOP ( 'NONE', ( #2820, #9251, #23967, #27928 ) ) ;
#34912=FACE_OUTER_BOUND ( 'NONE', #7318, .T. ) ;
#34918=AXIS2_PLACEMENT_3D ( 'NONE', #28022, #33411, #3712 ) ;
#34937=AXIS2_PLACEMENT_3D ( 'NONE', #25102, #31385, #20374 ) ;
#34939=AXIS2_PLACEMENT_3D ( 'NONE', #18561, #35146, #29563 ) ;
#34984=VECTOR ( 'NONE', #26531, 1000.000000000000000 ) ;
#35001=LINE ( 'NONE', #26713, #7248 ) ;
#35012=EDGE_CURVE ( 'NONE', #14425, #19237, #10745, .T. ) ;
#35025=EDGE_CURVE ( 'NONE', #23255, #27617, #1538, .T. ) ;
#35061=ORIENTED_EDGE ( 'NONE', *, *, #7627, .F. ) ;
#35068=ORIENTED_EDGE ( 'NONE', *, *, #7100, .T. ) ;
#35073=CIRCLE ( 'NONE', #1129, 4.800000000000000711 ) ;
#35074=CARTESIAN_POINT ( 'NONE',  ( 8.000000000000007105, -5.679790370316031733, 7.613867765417587030 ) ) ;
#35076=DIRECTION ( 'NONE',  ( -1.000000000000000000, 0.000000000000000000, 0.000000000000000000 ) ) ;
#35085=EDGE_CURVE ( 'NONE', #13957, #33344, #14784, .T. ) ;
#35120=DIRECTION ( 'NONE',  ( -1.000000000000000000, 0.000000000000000000, 0.000000000000000000 ) ) ;
#35130=EDGE_CURVE ( 'NONE', #4384, #22842, #34429, .T. ) ;
#35146=DIRECTION ( 'NONE',  ( -1.000000000000000000, 0.000000000000000000, 0.000000000000000000 ) ) ;
#35157=VERTEX_POINT ( 'NONE', #12633 ) ;
#35165=DIRECTION ( 'NONE',  ( -1.000000000000000000, 0.000000000000000000, 0.000000000000000000 ) ) ;
#35191=ORIENTED_EDGE ( 'NONE', *, *, #8077, .T. ) ;
#35196=DIRECTION ( 'NONE',  ( 1.000000000000000000, -0.000000000000000000, 0.000000000000000000 ) ) ;
#35209=CYLINDRICAL_SURFACE ( 'NONE', #33484, 4.800000000000000711 ) ;
#35218=AXIS2_PLACEMENT_3D ( 'NONE', #14697, #15051, #25711 ) ;
#35290=VECTOR ( 'NONE', #19627, 1000.000000000000000 ) ;
#35313=CARTESIAN_POINT ( 'NONE',  ( 4.000000000000003553, 10.15474465512060398, 9.637487275701170475 ) ) ;
#35315=ORIENTED_EDGE ( 'NONE', *, *, #17629, .T. ) ;
#35318=AXIS2_PLACEMENT_3D ( 'NONE', #13172, #18906, #10988 ) ;
#35342=ORIENTED_EDGE ( 'NONE', *, *, #9673, .T. ) ;
#35351=DIRECTION ( 'NONE',  ( 0.000000000000000000, 0.5000000000000009992, -0.8660254037844380415 ) ) ;
#35375=DIRECTION ( 'NONE',  ( 0.000000000000000000, -6.994405055138476738E-15, 1.000000000000000000 ) ) ;
#35412=DIRECTION ( 'NONE',  ( 0.000000000000000000, 1.000000000000000000, 3.497202527569241525E-15 ) ) ;
#35435=ORIENTED_EDGE ( 'NONE', *, *, #35012, .F. ) ;
#35442=AXIS2_PLACEMENT_3D ( 'NONE', #3418, #27889, #22120 ) ;
#35473=DIRECTION ( 'NONE',  ( 0.000000000000000000, 0.000000000000000000, 1.000000000000000000 ) ) ;
#35488=ORIENTED_EDGE ( 'NONE', *, *, #11651, .F. ) ;
#35504=VECTOR ( 'NONE', #9993, 1000.000000000000000 ) ;
#35542=EDGE_CURVE ( 'NONE', #16232, #14694, #15520, .T. ) ;
#35550=DIRECTION ( 'NONE',  ( -1.000000000000000000, 0.000000000000000000, 0.000000000000000000 ) ) ;
#35574=DIRECTION ( 'NONE',  ( 1.000000000000000000, -0.000000000000000000, -0.000000000000000000 ) ) ;
#35583=CIRCLE ( 'NONE', #25211, 4.800000000000005151 ) ;
#35599=DIRECTION ( 'NONE',  ( -1.000000000000000000, 0.000000000000000000, 0.000000000000000000 ) ) ;
#35612=LINE ( 'NONE', #25155, #21554 ) ;
ENDSEC;
END-ISO-10303-21;
